ISO-10303-21;
HEADER;
/* Generated by software containing ST-Developer
 * from STEP Tools, Inc. (www.steptools.com) 
 */
/* OPTION: using custom renumber hook */

FILE_DESCRIPTION(
/* description */ ('STEP AP242 Edition 2', 'CAx-IF Rec.Pracs.---Representation and Presentation of Product Manufa
cturing Information (PMI)---4.0---2014-10-13', 'CAx-IF Rec.Pracs.---3D Tessellated Geometry---0.4---2014-09-14', '2;1', 'CAx-IF Rec.Pracs.---User Defined Attributes---1.5---2016-08-15'),
/* implementation_level */ '2;1');

FILE_NAME(
/* name */ 'Nozzle cap.step',
/* time_stamp */ '2026-10-08T12:15:07Z',
/* author */ (''),
/* organization */ (''),
/* preprocessor_version */ 'ST-DEVELOPER v20',
/* originating_system */ 'ONSHAPE BY PTC INC, 1.221',
/* authorisation */ '  ');

FILE_SCHEMA (('AP242_MANAGED_MODEL_BASED_3D_ENGINEERING_MIM_LF { 1 0 10303 442 3 1 4 }'));
ENDSEC;

DATA;
#15=SPHERICAL_SURFACE('',#14380,0.001);
#63=COLOUR_RGB('', 0.08235294, 0.09019608, 0.10196078);
#212=SHAPE_REPRESENTATION_RELATIONSHIP('','',#13786,#239);
#239=ADVANCED_BREP_SHAPE_REPRESENTATION('',(#13730),#45476);
#315=TOROIDAL_SURFACE('',#14639,0.002,0.001);
#316=TOROIDAL_SURFACE('',#14640,0.00125,0.001);
#643=CIRCLE('',#14381,0.001);
#644=CIRCLE('',#14382,0.000625);
#645=CIRCLE('',#14387,0.0025);
#646=CIRCLE('',#14388,0.002);
#647=CIRCLE('',#14390,0.0045);
#648=CIRCLE('',#14391,0.0045);
#649=CIRCLE('',#14392,0.0045);
#650=CIRCLE('',#14393,0.0045);
#651=CIRCLE('',#14394,0.0045);
#652=CIRCLE('',#14395,0.0045);
#653=CIRCLE('',#14396,0.0045);
#654=CIRCLE('',#14397,0.0045);
#655=CIRCLE('',#14398,0.0045);
#656=CIRCLE('',#14399,0.0045);
#657=CIRCLE('',#14400,0.0045);
#658=CIRCLE('',#14401,0.0045);
#659=CIRCLE('',#14402,0.0045);
#660=CIRCLE('',#14403,0.0045);
#661=CIRCLE('',#14404,0.0045);
#662=CIRCLE('',#14405,0.0045);
#663=CIRCLE('',#14406,0.0045);
#664=CIRCLE('',#14407,0.0045);
#665=CIRCLE('',#14408,0.0045);
#666=CIRCLE('',#14409,0.0045);
#667=CIRCLE('',#14410,0.0045);
#668=CIRCLE('',#14411,0.0045);
#669=CIRCLE('',#14412,0.0045);
#670=CIRCLE('',#14413,0.0045);
#671=CIRCLE('',#14414,0.0045);
#672=CIRCLE('',#14415,0.0045);
#673=CIRCLE('',#14416,0.0045);
#674=CIRCLE('',#14417,0.0045);
#675=CIRCLE('',#14418,0.0045);
#676=CIRCLE('',#14419,0.0045);
#677=CIRCLE('',#14420,0.0045);
#678=CIRCLE('',#14421,0.0045);
#679=CIRCLE('',#14422,0.0045);
#680=CIRCLE('',#14423,0.0045);
#681=CIRCLE('',#14424,0.0045);
#682=CIRCLE('',#14425,0.0045);
#683=CIRCLE('',#14426,0.0045);
#684=CIRCLE('',#14427,0.0045);
#685=CIRCLE('',#14428,0.0045);
#686=CIRCLE('',#14429,0.0045);
#687=CIRCLE('',#14430,0.0045);
#688=CIRCLE('',#14431,0.0045);
#689=CIRCLE('',#14432,0.0045);
#690=CIRCLE('',#14433,0.0045);
#691=CIRCLE('',#14434,0.0045);
#692=CIRCLE('',#14435,0.0045);
#693=CIRCLE('',#14436,0.0045);
#694=CIRCLE('',#14437,0.00025);
#695=CIRCLE('',#14439,0.0045);
#696=CIRCLE('',#14440,0.0045);
#697=CIRCLE('',#14441,0.0045);
#698=CIRCLE('',#14442,0.0045);
#699=CIRCLE('',#14443,0.0045);
#700=CIRCLE('',#14444,0.0045);
#701=CIRCLE('',#14445,0.0045);
#702=CIRCLE('',#14446,0.0045);
#703=CIRCLE('',#14447,0.0045);
#704=CIRCLE('',#14448,0.0045);
#705=CIRCLE('',#14449,0.0045);
#706=CIRCLE('',#14450,0.0045);
#707=CIRCLE('',#14451,0.0045);
#708=CIRCLE('',#14452,0.0045);
#709=CIRCLE('',#14453,0.0045);
#710=CIRCLE('',#14454,0.0045);
#711=CIRCLE('',#14455,0.0045);
#712=CIRCLE('',#14456,0.0045);
#713=CIRCLE('',#14457,0.0045);
#714=CIRCLE('',#14458,0.0045);
#715=CIRCLE('',#14459,0.0045);
#716=CIRCLE('',#14460,0.0045);
#717=CIRCLE('',#14461,0.0045);
#718=CIRCLE('',#14462,0.0045);
#719=CIRCLE('',#14463,0.0045);
#720=CIRCLE('',#14464,0.0045);
#721=CIRCLE('',#14465,0.0045);
#722=CIRCLE('',#14466,0.0045);
#723=CIRCLE('',#14467,0.0045);
#724=CIRCLE('',#14468,0.0045);
#725=CIRCLE('',#14469,0.0045);
#726=CIRCLE('',#14470,0.0045);
#727=CIRCLE('',#14471,0.0045);
#728=CIRCLE('',#14472,0.0045);
#729=CIRCLE('',#14473,0.0045);
#730=CIRCLE('',#14474,0.0045);
#731=CIRCLE('',#14475,0.0045);
#732=CIRCLE('',#14476,0.0045);
#733=CIRCLE('',#14477,0.0045);
#734=CIRCLE('',#14478,0.0045);
#735=CIRCLE('',#14479,0.0045);
#736=CIRCLE('',#14480,0.0045);
#737=CIRCLE('',#14481,0.0045);
#738=CIRCLE('',#14482,0.0045);
#739=CIRCLE('',#14483,0.0045);
#740=CIRCLE('',#14484,0.0045);
#741=CIRCLE('',#14485,0.0045);
#742=CIRCLE('',#14486,0.004);
#743=CIRCLE('',#14631,0.0025);
#744=CIRCLE('',#14632,0.004);
#745=CIRCLE('',#14636,0.00025);
#746=CIRCLE('',#14638,0.001);
#1109=B_SPLINE_CURVE_WITH_KNOTS('',3,(#33682,#33683,#33684,#33685,#33686),
 .UNSPECIFIED.,.F.,.F.,(4,1,4),(1.76851098641564E-19,0.00223125534297384,
0.00446251068594769),.UNSPECIFIED.);
#1290=PLANE('',#14384);
#1291=PLANE('',#14385);
#1292=PLANE('',#14386);
#1293=PLANE('',#14389);
#1294=PLANE('',#14438);
#1295=PLANE('',#14488);
#1296=PLANE('',#14489);
#1297=PLANE('',#14491);
#1298=PLANE('',#14492);
#1299=PLANE('',#14494);
#1300=PLANE('',#14495);
#1301=PLANE('',#14497);
#1302=PLANE('',#14498);
#1303=PLANE('',#14500);
#1304=PLANE('',#14501);
#1305=PLANE('',#14503);
#1306=PLANE('',#14504);
#1307=PLANE('',#14506);
#1308=PLANE('',#14507);
#1309=PLANE('',#14509);
#1310=PLANE('',#14510);
#1311=PLANE('',#14512);
#1312=PLANE('',#14513);
#1313=PLANE('',#14515);
#1314=PLANE('',#14516);
#1315=PLANE('',#14518);
#1316=PLANE('',#14519);
#1317=PLANE('',#14521);
#1318=PLANE('',#14522);
#1319=PLANE('',#14524);
#1320=PLANE('',#14525);
#1321=PLANE('',#14527);
#1322=PLANE('',#14528);
#1323=PLANE('',#14530);
#1324=PLANE('',#14531);
#1325=PLANE('',#14533);
#1326=PLANE('',#14534);
#1327=PLANE('',#14536);
#1328=PLANE('',#14537);
#1329=PLANE('',#14539);
#1330=PLANE('',#14540);
#1331=PLANE('',#14542);
#1332=PLANE('',#14543);
#1333=PLANE('',#14545);
#1334=PLANE('',#14546);
#1335=PLANE('',#14548);
#1336=PLANE('',#14549);
#1337=PLANE('',#14551);
#1338=PLANE('',#14552);
#1339=PLANE('',#14554);
#1340=PLANE('',#14555);
#1341=PLANE('',#14557);
#1342=PLANE('',#14558);
#1343=PLANE('',#14560);
#1344=PLANE('',#14561);
#1345=PLANE('',#14563);
#1346=PLANE('',#14564);
#1347=PLANE('',#14566);
#1348=PLANE('',#14567);
#1349=PLANE('',#14569);
#1350=PLANE('',#14570);
#1351=PLANE('',#14572);
#1352=PLANE('',#14573);
#1353=PLANE('',#14575);
#1354=PLANE('',#14576);
#1355=PLANE('',#14578);
#1356=PLANE('',#14579);
#1357=PLANE('',#14581);
#1358=PLANE('',#14582);
#1359=PLANE('',#14584);
#1360=PLANE('',#14585);
#1361=PLANE('',#14587);
#1362=PLANE('',#14588);
#1363=PLANE('',#14590);
#1364=PLANE('',#14591);
#1365=PLANE('',#14593);
#1366=PLANE('',#14594);
#1367=PLANE('',#14596);
#1368=PLANE('',#14597);
#1369=PLANE('',#14599);
#1370=PLANE('',#14600);
#1371=PLANE('',#14602);
#1372=PLANE('',#14603);
#1373=PLANE('',#14605);
#1374=PLANE('',#14606);
#1375=PLANE('',#14608);
#1376=PLANE('',#14609);
#1377=PLANE('',#14611);
#1378=PLANE('',#14612);
#1379=PLANE('',#14614);
#1380=PLANE('',#14615);
#1381=PLANE('',#14616);
#1382=PLANE('',#14617);
#1383=PLANE('',#14619);
#1384=PLANE('',#14620);
#1385=PLANE('',#14622);
#1386=PLANE('',#14623);
#1387=PLANE('',#14625);
#1388=PLANE('',#14626);
#1389=PLANE('',#14628);
#1390=PLANE('',#14629);
#1391=PLANE('',#14630);
#1637=CYLINDRICAL_SURFACE('',#14383,0.00331189881249999);
#1638=CYLINDRICAL_SURFACE('',#14487,0.0045);
#1639=CYLINDRICAL_SURFACE('',#14490,0.0045);
#1640=CYLINDRICAL_SURFACE('',#14493,0.0045);
#1641=CYLINDRICAL_SURFACE('',#14496,0.0045);
#1642=CYLINDRICAL_SURFACE('',#14499,0.0045);
#1643=CYLINDRICAL_SURFACE('',#14502,0.0045);
#1644=CYLINDRICAL_SURFACE('',#14505,0.0045);
#1645=CYLINDRICAL_SURFACE('',#14508,0.0045);
#1646=CYLINDRICAL_SURFACE('',#14511,0.0045);
#1647=CYLINDRICAL_SURFACE('',#14514,0.0045);
#1648=CYLINDRICAL_SURFACE('',#14517,0.0045);
#1649=CYLINDRICAL_SURFACE('',#14520,0.0045);
#1650=CYLINDRICAL_SURFACE('',#14523,0.0045);
#1651=CYLINDRICAL_SURFACE('',#14526,0.0045);
#1652=CYLINDRICAL_SURFACE('',#14529,0.0045);
#1653=CYLINDRICAL_SURFACE('',#14532,0.0045);
#1654=CYLINDRICAL_SURFACE('',#14535,0.0045);
#1655=CYLINDRICAL_SURFACE('',#14538,0.0045);
#1656=CYLINDRICAL_SURFACE('',#14541,0.0045);
#1657=CYLINDRICAL_SURFACE('',#14544,0.0045);
#1658=CYLINDRICAL_SURFACE('',#14547,0.0045);
#1659=CYLINDRICAL_SURFACE('',#14550,0.0045);
#1660=CYLINDRICAL_SURFACE('',#14553,0.0045);
#1661=CYLINDRICAL_SURFACE('',#14556,0.0045);
#1662=CYLINDRICAL_SURFACE('',#14559,0.0045);
#1663=CYLINDRICAL_SURFACE('',#14562,0.0045);
#1664=CYLINDRICAL_SURFACE('',#14565,0.0045);
#1665=CYLINDRICAL_SURFACE('',#14568,0.0045);
#1666=CYLINDRICAL_SURFACE('',#14571,0.0045);
#1667=CYLINDRICAL_SURFACE('',#14574,0.0045);
#1668=CYLINDRICAL_SURFACE('',#14577,0.0045);
#1669=CYLINDRICAL_SURFACE('',#14580,0.0045);
#1670=CYLINDRICAL_SURFACE('',#14583,0.0045);
#1671=CYLINDRICAL_SURFACE('',#14586,0.0045);
#1672=CYLINDRICAL_SURFACE('',#14589,0.0045);
#1673=CYLINDRICAL_SURFACE('',#14592,0.0045);
#1674=CYLINDRICAL_SURFACE('',#14595,0.0045);
#1675=CYLINDRICAL_SURFACE('',#14598,0.0045);
#1676=CYLINDRICAL_SURFACE('',#14601,0.0045);
#1677=CYLINDRICAL_SURFACE('',#14604,0.0045);
#1678=CYLINDRICAL_SURFACE('',#14607,0.0045);
#1679=CYLINDRICAL_SURFACE('',#14610,0.0045);
#1680=CYLINDRICAL_SURFACE('',#14613,0.0045);
#1681=CYLINDRICAL_SURFACE('',#14618,0.0045);
#1682=CYLINDRICAL_SURFACE('',#14621,0.0045);
#1683=CYLINDRICAL_SURFACE('',#14624,0.0045);
#1684=CYLINDRICAL_SURFACE('',#14627,0.0045);
#1685=CYLINDRICAL_SURFACE('',#14633,0.0025);
#1686=CYLINDRICAL_SURFACE('',#14634,0.004);
#1687=CYLINDRICAL_SURFACE('',#14635,0.00025);
#1688=CYLINDRICAL_SURFACE('',#14637,0.001);
#1894=(
BOUNDED_CURVE()
B_SPLINE_CURVE(2,(#33689,#33690,#33691,#33692,#33693,#33694,#33695,#33696,
#33697),.UNSPECIFIED.,.F.,.F.)
B_SPLINE_CURVE_WITH_KNOTS((3,2,2,2,3),(0.6875,0.71875,0.75,0.78125,0.812500000739054),
 .UNSPECIFIED.)
CURVE()
GEOMETRIC_REPRESENTATION_ITEM()
RATIONAL_B_SPLINE_CURVE((1.,0.923879532511287,1.,0.923879532511287,1.,0.923879532511287,
1.,0.923879532511287,1.))
REPRESENTATION_ITEM('')
);
#1895=(
BOUNDED_CURVE()
B_SPLINE_CURVE(2,(#33699,#33700,#33701,#33702,#33703,#33704,#33705,#33706,
#33707),.UNSPECIFIED.,.F.,.F.)
B_SPLINE_CURVE_WITH_KNOTS((3,2,2,2,3),(0.5625,0.59375,0.625,0.65625,0.6875),
 .UNSPECIFIED.)
CURVE()
GEOMETRIC_REPRESENTATION_ITEM()
RATIONAL_B_SPLINE_CURVE((1.,0.923879532511287,1.,0.923879532511287,1.,0.923879532511287,
1.,0.923879532511287,1.))
REPRESENTATION_ITEM('')
);
#1896=(
BOUNDED_CURVE()
B_SPLINE_CURVE(2,(#33709,#33710,#33711,#33712,#33713,#33714,#33715,#33716,
#33717),.UNSPECIFIED.,.F.,.F.)
B_SPLINE_CURVE_WITH_KNOTS((3,2,2,2,3),(0.4375,0.46875,0.5,0.53125,0.5625),
 .UNSPECIFIED.)
CURVE()
GEOMETRIC_REPRESENTATION_ITEM()
RATIONAL_B_SPLINE_CURVE((1.,0.923879532511287,1.,0.923879532511287,1.,0.923879532511287,
1.,0.923879532511287,1.))
REPRESENTATION_ITEM('')
);
#1897=(
BOUNDED_CURVE()
B_SPLINE_CURVE(2,(#33719,#33720,#33721,#33722,#33723,#33724,#33725,#33726,
#33727),.UNSPECIFIED.,.F.,.F.)
B_SPLINE_CURVE_WITH_KNOTS((3,2,2,2,3),(0.3125,0.34375,0.375,0.40625,0.4375),
 .UNSPECIFIED.)
CURVE()
GEOMETRIC_REPRESENTATION_ITEM()
RATIONAL_B_SPLINE_CURVE((1.,0.923879532511287,1.,0.923879532511287,1.,0.923879532511287,
1.,0.923879532511287,1.))
REPRESENTATION_ITEM('')
);
#1898=(
BOUNDED_CURVE()
B_SPLINE_CURVE(2,(#33729,#33730,#33731,#33732,#33733,#33734,#33735,#33736,
#33737),.UNSPECIFIED.,.F.,.F.)
B_SPLINE_CURVE_WITH_KNOTS((3,2,2,2,3),(0.1875,0.21875,0.25,0.28125,0.3125),
 .UNSPECIFIED.)
CURVE()
GEOMETRIC_REPRESENTATION_ITEM()
RATIONAL_B_SPLINE_CURVE((1.,0.923879532511287,1.,0.923879532511287,1.,0.923879532511287,
1.,0.923879532511287,1.))
REPRESENTATION_ITEM('')
);
#1899=(
BOUNDED_CURVE()
B_SPLINE_CURVE(2,(#33739,#33740,#33741,#33742,#33743,#33744,#33745,#33746,
#33747),.UNSPECIFIED.,.F.,.F.)
B_SPLINE_CURVE_WITH_KNOTS((3,2,2,2,3),(0.0625,0.09375,0.125,0.15625,0.1875),
 .UNSPECIFIED.)
CURVE()
GEOMETRIC_REPRESENTATION_ITEM()
RATIONAL_B_SPLINE_CURVE((1.,0.923879532511287,1.,0.923879532511287,1.,0.923879532511287,
1.,0.923879532511287,1.))
REPRESENTATION_ITEM('')
);
#1900=(
BOUNDED_CURVE()
B_SPLINE_CURVE(2,(#33749,#33750,#33751,#33752,#33753),.UNSPECIFIED.,.F.,
 .F.)
B_SPLINE_CURVE_WITH_KNOTS((3,2,3),(0.,0.03125,0.0625),.UNSPECIFIED.)
CURVE()
GEOMETRIC_REPRESENTATION_ITEM()
RATIONAL_B_SPLINE_CURVE((1.,0.923879532511287,1.,0.923879532511287,1.))
REPRESENTATION_ITEM('')
);
#1901=(
BOUNDED_CURVE()
B_SPLINE_CURVE(2,(#33757,#33758,#33759,#33760,#33761,#33762,#33763,#33764,
#33765,#33766,#33767,#33768,#33769,#33770,#33771,#33772,#33773,#33774,#33775,
#33776,#33777,#33778,#33779,#33780,#33781,#33782,#33783,#33784,#33785,#33786,
#33787,#33788,#33789,#33790,#33791,#33792,#33793,#33794,#33795,#33796,#33797,
#33798,#33799,#33800,#33801,#33802,#33803,#33804,#33805,#33806,#33807,#33808,
#33809,#33810,#33811,#33812,#33813),.UNSPECIFIED.,.F.,.F.)
B_SPLINE_CURVE_WITH_KNOTS((3,2,2,2,2,2,2,2,2,2,2,2,2,2,2,2,2,2,2,2,2,2,
2,2,2,2,2,2,3),(0.,0.03125,0.0625,0.09375,0.125,0.15625,0.1875,0.21875,
0.25,0.28125,0.3125,0.34375,0.375,0.40625,0.4375,0.46875,0.5,0.53125,0.5625,
0.59375,0.625,0.65625,0.6875,0.71875,0.75,0.78125,0.8125,0.84375,0.875),
 .UNSPECIFIED.)
CURVE()
GEOMETRIC_REPRESENTATION_ITEM()
RATIONAL_B_SPLINE_CURVE((1.,0.923879532511287,1.,0.923879532511287,1.,0.923879532511287,
1.,0.923879532511287,1.,0.923879532511287,1.,0.923879532511287,1.,0.923879532511287,
1.,0.923879532511287,1.,0.923879532511287,1.,0.923879532511287,1.,0.923879532511287,
1.,0.923879532511287,1.,0.923879532511287,1.,0.923879532511287,1.,0.923879532511287,
1.,0.923879532511287,1.,0.923879532511287,1.,0.923879532511287,1.,0.923879532511287,
1.,0.923879532511287,1.,0.923879532511287,1.,0.923879532511287,1.,0.923879532511287,
1.,0.923879532511287,1.,0.923879532511287,1.,0.923879532511287,1.,0.923879532511287,
1.,0.923879532511287,1.))
REPRESENTATION_ITEM('')
);
#1902=(
BOUNDED_CURVE()
B_SPLINE_CURVE(2,(#33933,#33934,#33935,#33936,#33937),.UNSPECIFIED.,.F.,
 .F.)
B_SPLINE_CURVE_WITH_KNOTS((3,2,3),(0.,0.03125,0.0625),.UNSPECIFIED.)
CURVE()
GEOMETRIC_REPRESENTATION_ITEM()
RATIONAL_B_SPLINE_CURVE((1.,0.923879532511287,1.,0.923879532511287,1.))
REPRESENTATION_ITEM('')
);
#1903=(
BOUNDED_CURVE()
B_SPLINE_CURVE(2,(#33939,#33940,#33941,#33942,#33943,#33944,#33945,#33946,
#33947),.UNSPECIFIED.,.F.,.F.)
B_SPLINE_CURVE_WITH_KNOTS((3,2,2,2,3),(0.0625,0.09375,0.125,0.15625,0.1875),
 .UNSPECIFIED.)
CURVE()
GEOMETRIC_REPRESENTATION_ITEM()
RATIONAL_B_SPLINE_CURVE((1.,0.923879532511287,1.,0.923879532511287,1.,0.923879532511287,
1.,0.923879532511287,1.))
REPRESENTATION_ITEM('')
);
#1904=(
BOUNDED_CURVE()
B_SPLINE_CURVE(2,(#33949,#33950,#33951,#33952,#33953,#33954,#33955,#33956,
#33957),.UNSPECIFIED.,.F.,.F.)
B_SPLINE_CURVE_WITH_KNOTS((3,2,2,2,3),(0.1875,0.21875,0.25,0.28125,0.3125),
 .UNSPECIFIED.)
CURVE()
GEOMETRIC_REPRESENTATION_ITEM()
RATIONAL_B_SPLINE_CURVE((1.,0.923879532511287,1.,0.923879532511287,1.,0.923879532511287,
1.,0.923879532511287,1.))
REPRESENTATION_ITEM('')
);
#1905=(
BOUNDED_CURVE()
B_SPLINE_CURVE(2,(#33959,#33960,#33961,#33962,#33963,#33964,#33965,#33966,
#33967),.UNSPECIFIED.,.F.,.F.)
B_SPLINE_CURVE_WITH_KNOTS((3,2,2,2,3),(0.3125,0.34375,0.375,0.40625,0.4375),
 .UNSPECIFIED.)
CURVE()
GEOMETRIC_REPRESENTATION_ITEM()
RATIONAL_B_SPLINE_CURVE((1.,0.923879532511287,1.,0.923879532511287,1.,0.923879532511287,
1.,0.923879532511287,1.))
REPRESENTATION_ITEM('')
);
#1906=(
BOUNDED_CURVE()
B_SPLINE_CURVE(2,(#33969,#33970,#33971,#33972,#33973,#33974,#33975,#33976,
#33977),.UNSPECIFIED.,.F.,.F.)
B_SPLINE_CURVE_WITH_KNOTS((3,2,2,2,3),(0.4375,0.46875,0.5,0.53125,0.5625),
 .UNSPECIFIED.)
CURVE()
GEOMETRIC_REPRESENTATION_ITEM()
RATIONAL_B_SPLINE_CURVE((1.,0.923879532511287,1.,0.923879532511287,1.,0.923879532511287,
1.,0.923879532511287,1.))
REPRESENTATION_ITEM('')
);
#1907=(
BOUNDED_CURVE()
B_SPLINE_CURVE(2,(#33979,#33980,#33981,#33982,#33983,#33984,#33985,#33986,
#33987),.UNSPECIFIED.,.F.,.F.)
B_SPLINE_CURVE_WITH_KNOTS((3,2,2,2,3),(0.5625,0.59375,0.625,0.65625,0.6875),
 .UNSPECIFIED.)
CURVE()
GEOMETRIC_REPRESENTATION_ITEM()
RATIONAL_B_SPLINE_CURVE((1.,0.923879532511287,1.,0.923879532511287,1.,0.923879532511287,
1.,0.923879532511287,1.))
REPRESENTATION_ITEM('')
);
#1908=(
BOUNDED_CURVE()
B_SPLINE_CURVE(2,(#33989,#33990,#33991,#33992,#33993,#33994,#33995,#33996,
#33997),.UNSPECIFIED.,.F.,.F.)
B_SPLINE_CURVE_WITH_KNOTS((3,2,2,2,3),(0.6875,0.71875,0.75,0.78125,0.8125),
 .UNSPECIFIED.)
CURVE()
GEOMETRIC_REPRESENTATION_ITEM()
RATIONAL_B_SPLINE_CURVE((1.,0.923879532511287,1.,0.923879532511287,1.,0.923879532511287,
1.,0.923879532511287,1.))
REPRESENTATION_ITEM('')
);
#1909=(
BOUNDED_CURVE()
B_SPLINE_CURVE(2,(#33999,#34000,#34001,#34002,#34003),.UNSPECIFIED.,.F.,
 .F.)
B_SPLINE_CURVE_WITH_KNOTS((3,2,3),(0.8125,0.84375,0.875),.UNSPECIFIED.)
CURVE()
GEOMETRIC_REPRESENTATION_ITEM()
RATIONAL_B_SPLINE_CURVE((1.,0.923879532511287,1.,0.923879532511287,1.))
REPRESENTATION_ITEM('')
);
#1910=(
BOUNDED_CURVE()
B_SPLINE_CURVE(2,(#34007,#34008,#34009,#34010,#34011,#34012,#34013,#34014,
#34015,#34016,#34017,#34018,#34019,#34020,#34021,#34022,#34023,#34024,#34025,
#34026,#34027,#34028,#34029,#34030,#34031,#34032,#34033,#34034,#34035,#34036,
#34037,#34038,#34039,#34040,#34041,#34042,#34043,#34044,#34045,#34046,#34047,
#34048,#34049,#34050,#34051,#34052,#34053,#34054,#34055,#34056,#34057,#34058,
#34059,#34060,#34061,#34062,#34063),.UNSPECIFIED.,.F.,.F.)
B_SPLINE_CURVE_WITH_KNOTS((3,2,2,2,2,2,2,2,2,2,2,2,2,2,2,2,2,2,2,2,2,2,
2,2,2,2,2,2,3),(0.,0.03125,0.0625,0.09375,0.125,0.15625,0.1875,0.21875,
0.25,0.28125,0.3125,0.34375,0.375,0.40625,0.4375,0.46875,0.5,0.53125,0.5625,
0.59375,0.625,0.65625,0.6875,0.71875,0.75,0.78125,0.8125,0.84375,0.875),
 .UNSPECIFIED.)
CURVE()
GEOMETRIC_REPRESENTATION_ITEM()
RATIONAL_B_SPLINE_CURVE((1.,0.923879532511287,1.,0.923879532511287,1.,0.923879532511287,
1.,0.923879532511287,1.,0.923879532511287,1.,0.923879532511287,1.,0.923879532511287,
1.,0.923879532511287,1.,0.923879532511287,1.,0.923879532511287,1.,0.923879532511287,
1.,0.923879532511287,1.,0.923879532511287,1.,0.923879532511287,1.,0.923879532511287,
1.,0.923879532511287,1.,0.923879532511287,1.,0.923879532511287,1.,0.923879532511287,
1.,0.923879532511287,1.,0.923879532511287,1.,0.923879532511287,1.,0.923879532511287,
1.,0.923879532511287,1.,0.923879532511287,1.,0.923879532511287,1.,0.923879532511287,
1.,0.923879532511287,1.))
REPRESENTATION_ITEM('')
);
#3068=ORIENTED_EDGE('',*,*,#6181,.F.);
#3069=ORIENTED_EDGE('',*,*,#6182,.F.);
#3070=ORIENTED_EDGE('',*,*,#6183,.F.);
#3071=ORIENTED_EDGE('',*,*,#6184,.F.);
#3072=ORIENTED_EDGE('',*,*,#6185,.F.);
#3073=ORIENTED_EDGE('',*,*,#6186,.F.);
#3074=ORIENTED_EDGE('',*,*,#6187,.F.);
#3075=ORIENTED_EDGE('',*,*,#6188,.F.);
#3076=ORIENTED_EDGE('',*,*,#6189,.F.);
#3077=ORIENTED_EDGE('',*,*,#6190,.F.);
#3078=ORIENTED_EDGE('',*,*,#6191,.F.);
#3079=ORIENTED_EDGE('',*,*,#6192,.T.);
#3080=ORIENTED_EDGE('',*,*,#6193,.F.);
#3081=ORIENTED_EDGE('',*,*,#6194,.F.);
#3082=ORIENTED_EDGE('',*,*,#6195,.T.);
#3083=ORIENTED_EDGE('',*,*,#6196,.T.);
#3084=ORIENTED_EDGE('',*,*,#6197,.T.);
#3085=ORIENTED_EDGE('',*,*,#6198,.T.);
#3086=ORIENTED_EDGE('',*,*,#6199,.T.);
#3087=ORIENTED_EDGE('',*,*,#6200,.T.);
#3088=ORIENTED_EDGE('',*,*,#6201,.T.);
#3089=ORIENTED_EDGE('',*,*,#6202,.T.);
#3090=ORIENTED_EDGE('',*,*,#6203,.F.);
#3091=ORIENTED_EDGE('',*,*,#6204,.F.);
#3092=ORIENTED_EDGE('',*,*,#6205,.F.);
#3093=ORIENTED_EDGE('',*,*,#6204,.T.);
#3094=ORIENTED_EDGE('',*,*,#6206,.F.);
#3095=ORIENTED_EDGE('',*,*,#6192,.F.);
#3096=ORIENTED_EDGE('',*,*,#6207,.F.);
#3097=ORIENTED_EDGE('',*,*,#6193,.T.);
#3098=ORIENTED_EDGE('',*,*,#6206,.T.);
#3099=ORIENTED_EDGE('',*,*,#6203,.T.);
#3100=ORIENTED_EDGE('',*,*,#6208,.T.);
#3101=ORIENTED_EDGE('',*,*,#6205,.T.);
#3102=ORIENTED_EDGE('',*,*,#6191,.T.);
#3103=ORIENTED_EDGE('',*,*,#6209,.T.);
#3104=ORIENTED_EDGE('',*,*,#6194,.T.);
#3105=ORIENTED_EDGE('',*,*,#6210,.T.);
#3106=ORIENTED_EDGE('',*,*,#6211,.T.);
#3107=ORIENTED_EDGE('',*,*,#6212,.F.);
#3108=ORIENTED_EDGE('',*,*,#6213,.F.);
#3109=ORIENTED_EDGE('',*,*,#6214,.F.);
#3110=ORIENTED_EDGE('',*,*,#6215,.F.);
#3111=ORIENTED_EDGE('',*,*,#6216,.F.);
#3112=ORIENTED_EDGE('',*,*,#6217,.F.);
#3113=ORIENTED_EDGE('',*,*,#6218,.F.);
#3114=ORIENTED_EDGE('',*,*,#6219,.F.);
#3115=ORIENTED_EDGE('',*,*,#6220,.F.);
#3116=ORIENTED_EDGE('',*,*,#6221,.F.);
#3117=ORIENTED_EDGE('',*,*,#6222,.F.);
#3118=ORIENTED_EDGE('',*,*,#6223,.F.);
#3119=ORIENTED_EDGE('',*,*,#6224,.F.);
#3120=ORIENTED_EDGE('',*,*,#6225,.F.);
#3121=ORIENTED_EDGE('',*,*,#6226,.F.);
#3122=ORIENTED_EDGE('',*,*,#6227,.F.);
#3123=ORIENTED_EDGE('',*,*,#6228,.F.);
#3124=ORIENTED_EDGE('',*,*,#6229,.F.);
#3125=ORIENTED_EDGE('',*,*,#6230,.F.);
#3126=ORIENTED_EDGE('',*,*,#6231,.F.);
#3127=ORIENTED_EDGE('',*,*,#6232,.F.);
#3128=ORIENTED_EDGE('',*,*,#6233,.F.);
#3129=ORIENTED_EDGE('',*,*,#6234,.F.);
#3130=ORIENTED_EDGE('',*,*,#6235,.F.);
#3131=ORIENTED_EDGE('',*,*,#6236,.F.);
#3132=ORIENTED_EDGE('',*,*,#6237,.F.);
#3133=ORIENTED_EDGE('',*,*,#6238,.F.);
#3134=ORIENTED_EDGE('',*,*,#6239,.F.);
#3135=ORIENTED_EDGE('',*,*,#6240,.F.);
#3136=ORIENTED_EDGE('',*,*,#6241,.F.);
#3137=ORIENTED_EDGE('',*,*,#6242,.F.);
#3138=ORIENTED_EDGE('',*,*,#6243,.F.);
#3139=ORIENTED_EDGE('',*,*,#6244,.F.);
#3140=ORIENTED_EDGE('',*,*,#6245,.F.);
#3141=ORIENTED_EDGE('',*,*,#6246,.F.);
#3142=ORIENTED_EDGE('',*,*,#6247,.F.);
#3143=ORIENTED_EDGE('',*,*,#6248,.F.);
#3144=ORIENTED_EDGE('',*,*,#6249,.F.);
#3145=ORIENTED_EDGE('',*,*,#6250,.F.);
#3146=ORIENTED_EDGE('',*,*,#6251,.F.);
#3147=ORIENTED_EDGE('',*,*,#6252,.F.);
#3148=ORIENTED_EDGE('',*,*,#6253,.F.);
#3149=ORIENTED_EDGE('',*,*,#6254,.F.);
#3150=ORIENTED_EDGE('',*,*,#6255,.F.);
#3151=ORIENTED_EDGE('',*,*,#6256,.F.);
#3152=ORIENTED_EDGE('',*,*,#6257,.F.);
#3153=ORIENTED_EDGE('',*,*,#6258,.F.);
#3154=ORIENTED_EDGE('',*,*,#6259,.F.);
#3155=ORIENTED_EDGE('',*,*,#6260,.F.);
#3156=ORIENTED_EDGE('',*,*,#6261,.F.);
#3157=ORIENTED_EDGE('',*,*,#6262,.F.);
#3158=ORIENTED_EDGE('',*,*,#6263,.F.);
#3159=ORIENTED_EDGE('',*,*,#6264,.F.);
#3160=ORIENTED_EDGE('',*,*,#6265,.F.);
#3161=ORIENTED_EDGE('',*,*,#6266,.F.);
#3162=ORIENTED_EDGE('',*,*,#6267,.F.);
#3163=ORIENTED_EDGE('',*,*,#6268,.F.);
#3164=ORIENTED_EDGE('',*,*,#6269,.F.);
#3165=ORIENTED_EDGE('',*,*,#6270,.F.);
#3166=ORIENTED_EDGE('',*,*,#6271,.F.);
#3167=ORIENTED_EDGE('',*,*,#6272,.F.);
#3168=ORIENTED_EDGE('',*,*,#6273,.F.);
#3169=ORIENTED_EDGE('',*,*,#6274,.F.);
#3170=ORIENTED_EDGE('',*,*,#6275,.F.);
#3171=ORIENTED_EDGE('',*,*,#6276,.F.);
#3172=ORIENTED_EDGE('',*,*,#6277,.F.);
#3173=ORIENTED_EDGE('',*,*,#6278,.F.);
#3174=ORIENTED_EDGE('',*,*,#6279,.F.);
#3175=ORIENTED_EDGE('',*,*,#6280,.F.);
#3176=ORIENTED_EDGE('',*,*,#6281,.F.);
#3177=ORIENTED_EDGE('',*,*,#6282,.F.);
#3178=ORIENTED_EDGE('',*,*,#6283,.F.);
#3179=ORIENTED_EDGE('',*,*,#6284,.F.);
#3180=ORIENTED_EDGE('',*,*,#6285,.F.);
#3181=ORIENTED_EDGE('',*,*,#6286,.F.);
#3182=ORIENTED_EDGE('',*,*,#6287,.F.);
#3183=ORIENTED_EDGE('',*,*,#6288,.F.);
#3184=ORIENTED_EDGE('',*,*,#6289,.F.);
#3185=ORIENTED_EDGE('',*,*,#6290,.F.);
#3186=ORIENTED_EDGE('',*,*,#6291,.F.);
#3187=ORIENTED_EDGE('',*,*,#6292,.F.);
#3188=ORIENTED_EDGE('',*,*,#6293,.F.);
#3189=ORIENTED_EDGE('',*,*,#6294,.F.);
#3190=ORIENTED_EDGE('',*,*,#6295,.F.);
#3191=ORIENTED_EDGE('',*,*,#6296,.F.);
#3192=ORIENTED_EDGE('',*,*,#6297,.F.);
#3193=ORIENTED_EDGE('',*,*,#6298,.F.);
#3194=ORIENTED_EDGE('',*,*,#6299,.F.);
#3195=ORIENTED_EDGE('',*,*,#6300,.F.);
#3196=ORIENTED_EDGE('',*,*,#6301,.F.);
#3197=ORIENTED_EDGE('',*,*,#6302,.F.);
#3198=ORIENTED_EDGE('',*,*,#6303,.F.);
#3199=ORIENTED_EDGE('',*,*,#6304,.F.);
#3200=ORIENTED_EDGE('',*,*,#6305,.F.);
#3201=ORIENTED_EDGE('',*,*,#6306,.F.);
#3202=ORIENTED_EDGE('',*,*,#6307,.F.);
#3203=ORIENTED_EDGE('',*,*,#6308,.F.);
#3204=ORIENTED_EDGE('',*,*,#6309,.F.);
#3205=ORIENTED_EDGE('',*,*,#6310,.F.);
#3206=ORIENTED_EDGE('',*,*,#6311,.F.);
#3207=ORIENTED_EDGE('',*,*,#6312,.F.);
#3208=ORIENTED_EDGE('',*,*,#6313,.F.);
#3209=ORIENTED_EDGE('',*,*,#6314,.F.);
#3210=ORIENTED_EDGE('',*,*,#6315,.F.);
#3211=ORIENTED_EDGE('',*,*,#6316,.F.);
#3212=ORIENTED_EDGE('',*,*,#6317,.F.);
#3213=ORIENTED_EDGE('',*,*,#6318,.F.);
#3214=ORIENTED_EDGE('',*,*,#6319,.F.);
#3215=ORIENTED_EDGE('',*,*,#6320,.F.);
#3216=ORIENTED_EDGE('',*,*,#6321,.F.);
#3217=ORIENTED_EDGE('',*,*,#6322,.F.);
#3218=ORIENTED_EDGE('',*,*,#6323,.F.);
#3219=ORIENTED_EDGE('',*,*,#6324,.F.);
#3220=ORIENTED_EDGE('',*,*,#6325,.F.);
#3221=ORIENTED_EDGE('',*,*,#6326,.F.);
#3222=ORIENTED_EDGE('',*,*,#6327,.F.);
#3223=ORIENTED_EDGE('',*,*,#6328,.F.);
#3224=ORIENTED_EDGE('',*,*,#6329,.F.);
#3225=ORIENTED_EDGE('',*,*,#6330,.F.);
#3226=ORIENTED_EDGE('',*,*,#6331,.F.);
#3227=ORIENTED_EDGE('',*,*,#6332,.F.);
#3228=ORIENTED_EDGE('',*,*,#6333,.F.);
#3229=ORIENTED_EDGE('',*,*,#6334,.F.);
#3230=ORIENTED_EDGE('',*,*,#6335,.F.);
#3231=ORIENTED_EDGE('',*,*,#6336,.F.);
#3232=ORIENTED_EDGE('',*,*,#6337,.F.);
#3233=ORIENTED_EDGE('',*,*,#6338,.F.);
#3234=ORIENTED_EDGE('',*,*,#6339,.F.);
#3235=ORIENTED_EDGE('',*,*,#6340,.F.);
#3236=ORIENTED_EDGE('',*,*,#6341,.F.);
#3237=ORIENTED_EDGE('',*,*,#6342,.F.);
#3238=ORIENTED_EDGE('',*,*,#6343,.F.);
#3239=ORIENTED_EDGE('',*,*,#6344,.F.);
#3240=ORIENTED_EDGE('',*,*,#6345,.F.);
#3241=ORIENTED_EDGE('',*,*,#6346,.F.);
#3242=ORIENTED_EDGE('',*,*,#6347,.F.);
#3243=ORIENTED_EDGE('',*,*,#6348,.F.);
#3244=ORIENTED_EDGE('',*,*,#6349,.F.);
#3245=ORIENTED_EDGE('',*,*,#6350,.F.);
#3246=ORIENTED_EDGE('',*,*,#6351,.F.);
#3247=ORIENTED_EDGE('',*,*,#6352,.F.);
#3248=ORIENTED_EDGE('',*,*,#6353,.F.);
#3249=ORIENTED_EDGE('',*,*,#6354,.F.);
#3250=ORIENTED_EDGE('',*,*,#6355,.F.);
#3251=ORIENTED_EDGE('',*,*,#6356,.T.);
#3252=ORIENTED_EDGE('',*,*,#6357,.T.);
#3253=ORIENTED_EDGE('',*,*,#6358,.T.);
#3254=ORIENTED_EDGE('',*,*,#6359,.T.);
#3255=ORIENTED_EDGE('',*,*,#6360,.T.);
#3256=ORIENTED_EDGE('',*,*,#6361,.T.);
#3257=ORIENTED_EDGE('',*,*,#6362,.T.);
#3258=ORIENTED_EDGE('',*,*,#6363,.T.);
#3259=ORIENTED_EDGE('',*,*,#6364,.T.);
#3260=ORIENTED_EDGE('',*,*,#6365,.T.);
#3261=ORIENTED_EDGE('',*,*,#6366,.T.);
#3262=ORIENTED_EDGE('',*,*,#6367,.T.);
#3263=ORIENTED_EDGE('',*,*,#6368,.T.);
#3264=ORIENTED_EDGE('',*,*,#6369,.T.);
#3265=ORIENTED_EDGE('',*,*,#6370,.T.);
#3266=ORIENTED_EDGE('',*,*,#6371,.T.);
#3267=ORIENTED_EDGE('',*,*,#6372,.T.);
#3268=ORIENTED_EDGE('',*,*,#6373,.T.);
#3269=ORIENTED_EDGE('',*,*,#6374,.T.);
#3270=ORIENTED_EDGE('',*,*,#6375,.T.);
#3271=ORIENTED_EDGE('',*,*,#6376,.T.);
#3272=ORIENTED_EDGE('',*,*,#6377,.T.);
#3273=ORIENTED_EDGE('',*,*,#6378,.T.);
#3274=ORIENTED_EDGE('',*,*,#6379,.T.);
#3275=ORIENTED_EDGE('',*,*,#6380,.T.);
#3276=ORIENTED_EDGE('',*,*,#6381,.T.);
#3277=ORIENTED_EDGE('',*,*,#6382,.T.);
#3278=ORIENTED_EDGE('',*,*,#6383,.T.);
#3279=ORIENTED_EDGE('',*,*,#6384,.T.);
#3280=ORIENTED_EDGE('',*,*,#6385,.T.);
#3281=ORIENTED_EDGE('',*,*,#6386,.T.);
#3282=ORIENTED_EDGE('',*,*,#6387,.T.);
#3283=ORIENTED_EDGE('',*,*,#6388,.T.);
#3284=ORIENTED_EDGE('',*,*,#6389,.T.);
#3285=ORIENTED_EDGE('',*,*,#6390,.T.);
#3286=ORIENTED_EDGE('',*,*,#6391,.T.);
#3287=ORIENTED_EDGE('',*,*,#6392,.T.);
#3288=ORIENTED_EDGE('',*,*,#6393,.T.);
#3289=ORIENTED_EDGE('',*,*,#6394,.T.);
#3290=ORIENTED_EDGE('',*,*,#6395,.T.);
#3291=ORIENTED_EDGE('',*,*,#6396,.T.);
#3292=ORIENTED_EDGE('',*,*,#6397,.T.);
#3293=ORIENTED_EDGE('',*,*,#6398,.T.);
#3294=ORIENTED_EDGE('',*,*,#6399,.T.);
#3295=ORIENTED_EDGE('',*,*,#6400,.T.);
#3296=ORIENTED_EDGE('',*,*,#6401,.T.);
#3297=ORIENTED_EDGE('',*,*,#6402,.T.);
#3298=ORIENTED_EDGE('',*,*,#6403,.T.);
#3299=ORIENTED_EDGE('',*,*,#6404,.T.);
#3300=ORIENTED_EDGE('',*,*,#6405,.T.);
#3301=ORIENTED_EDGE('',*,*,#6406,.T.);
#3302=ORIENTED_EDGE('',*,*,#6407,.T.);
#3303=ORIENTED_EDGE('',*,*,#6408,.T.);
#3304=ORIENTED_EDGE('',*,*,#6409,.T.);
#3305=ORIENTED_EDGE('',*,*,#6410,.T.);
#3306=ORIENTED_EDGE('',*,*,#6411,.T.);
#3307=ORIENTED_EDGE('',*,*,#6412,.T.);
#3308=ORIENTED_EDGE('',*,*,#6413,.T.);
#3309=ORIENTED_EDGE('',*,*,#6414,.T.);
#3310=ORIENTED_EDGE('',*,*,#6415,.T.);
#3311=ORIENTED_EDGE('',*,*,#6416,.T.);
#3312=ORIENTED_EDGE('',*,*,#6417,.T.);
#3313=ORIENTED_EDGE('',*,*,#6418,.T.);
#3314=ORIENTED_EDGE('',*,*,#6419,.T.);
#3315=ORIENTED_EDGE('',*,*,#6420,.T.);
#3316=ORIENTED_EDGE('',*,*,#6421,.T.);
#3317=ORIENTED_EDGE('',*,*,#6422,.T.);
#3318=ORIENTED_EDGE('',*,*,#6423,.T.);
#3319=ORIENTED_EDGE('',*,*,#6424,.T.);
#3320=ORIENTED_EDGE('',*,*,#6425,.T.);
#3321=ORIENTED_EDGE('',*,*,#6426,.T.);
#3322=ORIENTED_EDGE('',*,*,#6427,.T.);
#3323=ORIENTED_EDGE('',*,*,#6428,.T.);
#3324=ORIENTED_EDGE('',*,*,#6429,.T.);
#3325=ORIENTED_EDGE('',*,*,#6430,.T.);
#3326=ORIENTED_EDGE('',*,*,#6431,.T.);
#3327=ORIENTED_EDGE('',*,*,#6432,.T.);
#3328=ORIENTED_EDGE('',*,*,#6433,.T.);
#3329=ORIENTED_EDGE('',*,*,#6434,.T.);
#3330=ORIENTED_EDGE('',*,*,#6435,.T.);
#3331=ORIENTED_EDGE('',*,*,#6436,.T.);
#3332=ORIENTED_EDGE('',*,*,#6437,.T.);
#3333=ORIENTED_EDGE('',*,*,#6438,.T.);
#3334=ORIENTED_EDGE('',*,*,#6439,.T.);
#3335=ORIENTED_EDGE('',*,*,#6440,.T.);
#3336=ORIENTED_EDGE('',*,*,#6441,.T.);
#3337=ORIENTED_EDGE('',*,*,#6442,.T.);
#3338=ORIENTED_EDGE('',*,*,#6443,.T.);
#3339=ORIENTED_EDGE('',*,*,#6444,.T.);
#3340=ORIENTED_EDGE('',*,*,#6445,.T.);
#3341=ORIENTED_EDGE('',*,*,#6446,.T.);
#3342=ORIENTED_EDGE('',*,*,#6447,.T.);
#3343=ORIENTED_EDGE('',*,*,#6448,.T.);
#3344=ORIENTED_EDGE('',*,*,#6449,.T.);
#3345=ORIENTED_EDGE('',*,*,#6450,.T.);
#3346=ORIENTED_EDGE('',*,*,#6451,.T.);
#3347=ORIENTED_EDGE('',*,*,#6452,.T.);
#3348=ORIENTED_EDGE('',*,*,#6453,.T.);
#3349=ORIENTED_EDGE('',*,*,#6454,.T.);
#3350=ORIENTED_EDGE('',*,*,#6455,.T.);
#3351=ORIENTED_EDGE('',*,*,#6456,.T.);
#3352=ORIENTED_EDGE('',*,*,#6457,.T.);
#3353=ORIENTED_EDGE('',*,*,#6458,.T.);
#3354=ORIENTED_EDGE('',*,*,#6459,.T.);
#3355=ORIENTED_EDGE('',*,*,#6460,.T.);
#3356=ORIENTED_EDGE('',*,*,#6461,.T.);
#3357=ORIENTED_EDGE('',*,*,#6462,.T.);
#3358=ORIENTED_EDGE('',*,*,#6463,.T.);
#3359=ORIENTED_EDGE('',*,*,#6464,.T.);
#3360=ORIENTED_EDGE('',*,*,#6465,.T.);
#3361=ORIENTED_EDGE('',*,*,#6466,.T.);
#3362=ORIENTED_EDGE('',*,*,#6467,.T.);
#3363=ORIENTED_EDGE('',*,*,#6468,.T.);
#3364=ORIENTED_EDGE('',*,*,#6469,.T.);
#3365=ORIENTED_EDGE('',*,*,#6470,.T.);
#3366=ORIENTED_EDGE('',*,*,#6471,.T.);
#3367=ORIENTED_EDGE('',*,*,#6472,.T.);
#3368=ORIENTED_EDGE('',*,*,#6473,.T.);
#3369=ORIENTED_EDGE('',*,*,#6474,.T.);
#3370=ORIENTED_EDGE('',*,*,#6475,.T.);
#3371=ORIENTED_EDGE('',*,*,#6476,.T.);
#3372=ORIENTED_EDGE('',*,*,#6477,.T.);
#3373=ORIENTED_EDGE('',*,*,#6478,.T.);
#3374=ORIENTED_EDGE('',*,*,#6479,.T.);
#3375=ORIENTED_EDGE('',*,*,#6480,.T.);
#3376=ORIENTED_EDGE('',*,*,#6481,.T.);
#3377=ORIENTED_EDGE('',*,*,#6482,.T.);
#3378=ORIENTED_EDGE('',*,*,#6483,.T.);
#3379=ORIENTED_EDGE('',*,*,#6484,.T.);
#3380=ORIENTED_EDGE('',*,*,#6485,.T.);
#3381=ORIENTED_EDGE('',*,*,#6486,.T.);
#3382=ORIENTED_EDGE('',*,*,#6487,.T.);
#3383=ORIENTED_EDGE('',*,*,#6488,.T.);
#3384=ORIENTED_EDGE('',*,*,#6489,.T.);
#3385=ORIENTED_EDGE('',*,*,#6490,.T.);
#3386=ORIENTED_EDGE('',*,*,#6491,.T.);
#3387=ORIENTED_EDGE('',*,*,#6492,.T.);
#3388=ORIENTED_EDGE('',*,*,#6493,.T.);
#3389=ORIENTED_EDGE('',*,*,#6494,.T.);
#3390=ORIENTED_EDGE('',*,*,#6495,.T.);
#3391=ORIENTED_EDGE('',*,*,#6496,.T.);
#3392=ORIENTED_EDGE('',*,*,#6497,.T.);
#3393=ORIENTED_EDGE('',*,*,#6498,.T.);
#3394=ORIENTED_EDGE('',*,*,#6499,.F.);
#3395=ORIENTED_EDGE('',*,*,#6213,.T.);
#3396=ORIENTED_EDGE('',*,*,#6500,.F.);
#3397=ORIENTED_EDGE('',*,*,#6498,.F.);
#3398=ORIENTED_EDGE('',*,*,#6501,.T.);
#3399=ORIENTED_EDGE('',*,*,#6214,.T.);
#3400=ORIENTED_EDGE('',*,*,#6501,.F.);
#3401=ORIENTED_EDGE('',*,*,#6497,.F.);
#3402=ORIENTED_EDGE('',*,*,#6502,.T.);
#3403=ORIENTED_EDGE('',*,*,#6215,.T.);
#3404=ORIENTED_EDGE('',*,*,#6502,.F.);
#3405=ORIENTED_EDGE('',*,*,#6496,.F.);
#3406=ORIENTED_EDGE('',*,*,#6503,.T.);
#3407=ORIENTED_EDGE('',*,*,#6216,.T.);
#3408=ORIENTED_EDGE('',*,*,#6503,.F.);
#3409=ORIENTED_EDGE('',*,*,#6495,.F.);
#3410=ORIENTED_EDGE('',*,*,#6504,.T.);
#3411=ORIENTED_EDGE('',*,*,#6217,.T.);
#3412=ORIENTED_EDGE('',*,*,#6504,.F.);
#3413=ORIENTED_EDGE('',*,*,#6494,.F.);
#3414=ORIENTED_EDGE('',*,*,#6505,.T.);
#3415=ORIENTED_EDGE('',*,*,#6218,.T.);
#3416=ORIENTED_EDGE('',*,*,#6505,.F.);
#3417=ORIENTED_EDGE('',*,*,#6493,.F.);
#3418=ORIENTED_EDGE('',*,*,#6506,.T.);
#3419=ORIENTED_EDGE('',*,*,#6219,.T.);
#3420=ORIENTED_EDGE('',*,*,#6506,.F.);
#3421=ORIENTED_EDGE('',*,*,#6492,.F.);
#3422=ORIENTED_EDGE('',*,*,#6507,.T.);
#3423=ORIENTED_EDGE('',*,*,#6220,.T.);
#3424=ORIENTED_EDGE('',*,*,#6507,.F.);
#3425=ORIENTED_EDGE('',*,*,#6491,.F.);
#3426=ORIENTED_EDGE('',*,*,#6508,.T.);
#3427=ORIENTED_EDGE('',*,*,#6221,.T.);
#3428=ORIENTED_EDGE('',*,*,#6508,.F.);
#3429=ORIENTED_EDGE('',*,*,#6490,.F.);
#3430=ORIENTED_EDGE('',*,*,#6509,.T.);
#3431=ORIENTED_EDGE('',*,*,#6222,.T.);
#3432=ORIENTED_EDGE('',*,*,#6509,.F.);
#3433=ORIENTED_EDGE('',*,*,#6489,.F.);
#3434=ORIENTED_EDGE('',*,*,#6510,.T.);
#3435=ORIENTED_EDGE('',*,*,#6223,.T.);
#3436=ORIENTED_EDGE('',*,*,#6510,.F.);
#3437=ORIENTED_EDGE('',*,*,#6488,.F.);
#3438=ORIENTED_EDGE('',*,*,#6511,.T.);
#3439=ORIENTED_EDGE('',*,*,#6224,.T.);
#3440=ORIENTED_EDGE('',*,*,#6511,.F.);
#3441=ORIENTED_EDGE('',*,*,#6487,.F.);
#3442=ORIENTED_EDGE('',*,*,#6512,.T.);
#3443=ORIENTED_EDGE('',*,*,#6225,.T.);
#3444=ORIENTED_EDGE('',*,*,#6512,.F.);
#3445=ORIENTED_EDGE('',*,*,#6486,.F.);
#3446=ORIENTED_EDGE('',*,*,#6513,.T.);
#3447=ORIENTED_EDGE('',*,*,#6226,.T.);
#3448=ORIENTED_EDGE('',*,*,#6513,.F.);
#3449=ORIENTED_EDGE('',*,*,#6485,.F.);
#3450=ORIENTED_EDGE('',*,*,#6514,.T.);
#3451=ORIENTED_EDGE('',*,*,#6227,.T.);
#3452=ORIENTED_EDGE('',*,*,#6514,.F.);
#3453=ORIENTED_EDGE('',*,*,#6484,.F.);
#3454=ORIENTED_EDGE('',*,*,#6515,.T.);
#3455=ORIENTED_EDGE('',*,*,#6228,.T.);
#3456=ORIENTED_EDGE('',*,*,#6515,.F.);
#3457=ORIENTED_EDGE('',*,*,#6483,.F.);
#3458=ORIENTED_EDGE('',*,*,#6516,.T.);
#3459=ORIENTED_EDGE('',*,*,#6229,.T.);
#3460=ORIENTED_EDGE('',*,*,#6516,.F.);
#3461=ORIENTED_EDGE('',*,*,#6482,.F.);
#3462=ORIENTED_EDGE('',*,*,#6517,.T.);
#3463=ORIENTED_EDGE('',*,*,#6230,.T.);
#3464=ORIENTED_EDGE('',*,*,#6517,.F.);
#3465=ORIENTED_EDGE('',*,*,#6481,.F.);
#3466=ORIENTED_EDGE('',*,*,#6518,.T.);
#3467=ORIENTED_EDGE('',*,*,#6231,.T.);
#3468=ORIENTED_EDGE('',*,*,#6518,.F.);
#3469=ORIENTED_EDGE('',*,*,#6480,.F.);
#3470=ORIENTED_EDGE('',*,*,#6519,.T.);
#3471=ORIENTED_EDGE('',*,*,#6232,.T.);
#3472=ORIENTED_EDGE('',*,*,#6519,.F.);
#3473=ORIENTED_EDGE('',*,*,#6479,.F.);
#3474=ORIENTED_EDGE('',*,*,#6520,.T.);
#3475=ORIENTED_EDGE('',*,*,#6233,.T.);
#3476=ORIENTED_EDGE('',*,*,#6520,.F.);
#3477=ORIENTED_EDGE('',*,*,#6478,.F.);
#3478=ORIENTED_EDGE('',*,*,#6521,.T.);
#3479=ORIENTED_EDGE('',*,*,#6234,.T.);
#3480=ORIENTED_EDGE('',*,*,#6521,.F.);
#3481=ORIENTED_EDGE('',*,*,#6477,.F.);
#3482=ORIENTED_EDGE('',*,*,#6522,.T.);
#3483=ORIENTED_EDGE('',*,*,#6235,.T.);
#3484=ORIENTED_EDGE('',*,*,#6522,.F.);
#3485=ORIENTED_EDGE('',*,*,#6476,.F.);
#3486=ORIENTED_EDGE('',*,*,#6523,.T.);
#3487=ORIENTED_EDGE('',*,*,#6236,.T.);
#3488=ORIENTED_EDGE('',*,*,#6523,.F.);
#3489=ORIENTED_EDGE('',*,*,#6475,.F.);
#3490=ORIENTED_EDGE('',*,*,#6524,.T.);
#3491=ORIENTED_EDGE('',*,*,#6237,.T.);
#3492=ORIENTED_EDGE('',*,*,#6524,.F.);
#3493=ORIENTED_EDGE('',*,*,#6474,.F.);
#3494=ORIENTED_EDGE('',*,*,#6525,.T.);
#3495=ORIENTED_EDGE('',*,*,#6238,.T.);
#3496=ORIENTED_EDGE('',*,*,#6525,.F.);
#3497=ORIENTED_EDGE('',*,*,#6473,.F.);
#3498=ORIENTED_EDGE('',*,*,#6526,.T.);
#3499=ORIENTED_EDGE('',*,*,#6239,.T.);
#3500=ORIENTED_EDGE('',*,*,#6526,.F.);
#3501=ORIENTED_EDGE('',*,*,#6472,.F.);
#3502=ORIENTED_EDGE('',*,*,#6527,.T.);
#3503=ORIENTED_EDGE('',*,*,#6240,.T.);
#3504=ORIENTED_EDGE('',*,*,#6527,.F.);
#3505=ORIENTED_EDGE('',*,*,#6471,.F.);
#3506=ORIENTED_EDGE('',*,*,#6528,.T.);
#3507=ORIENTED_EDGE('',*,*,#6241,.T.);
#3508=ORIENTED_EDGE('',*,*,#6528,.F.);
#3509=ORIENTED_EDGE('',*,*,#6470,.F.);
#3510=ORIENTED_EDGE('',*,*,#6529,.T.);
#3511=ORIENTED_EDGE('',*,*,#6242,.T.);
#3512=ORIENTED_EDGE('',*,*,#6529,.F.);
#3513=ORIENTED_EDGE('',*,*,#6469,.F.);
#3514=ORIENTED_EDGE('',*,*,#6530,.T.);
#3515=ORIENTED_EDGE('',*,*,#6243,.T.);
#3516=ORIENTED_EDGE('',*,*,#6530,.F.);
#3517=ORIENTED_EDGE('',*,*,#6468,.F.);
#3518=ORIENTED_EDGE('',*,*,#6531,.T.);
#3519=ORIENTED_EDGE('',*,*,#6244,.T.);
#3520=ORIENTED_EDGE('',*,*,#6531,.F.);
#3521=ORIENTED_EDGE('',*,*,#6467,.F.);
#3522=ORIENTED_EDGE('',*,*,#6532,.T.);
#3523=ORIENTED_EDGE('',*,*,#6245,.T.);
#3524=ORIENTED_EDGE('',*,*,#6532,.F.);
#3525=ORIENTED_EDGE('',*,*,#6466,.F.);
#3526=ORIENTED_EDGE('',*,*,#6533,.T.);
#3527=ORIENTED_EDGE('',*,*,#6246,.T.);
#3528=ORIENTED_EDGE('',*,*,#6533,.F.);
#3529=ORIENTED_EDGE('',*,*,#6465,.F.);
#3530=ORIENTED_EDGE('',*,*,#6534,.T.);
#3531=ORIENTED_EDGE('',*,*,#6247,.T.);
#3532=ORIENTED_EDGE('',*,*,#6534,.F.);
#3533=ORIENTED_EDGE('',*,*,#6464,.F.);
#3534=ORIENTED_EDGE('',*,*,#6535,.T.);
#3535=ORIENTED_EDGE('',*,*,#6248,.T.);
#3536=ORIENTED_EDGE('',*,*,#6535,.F.);
#3537=ORIENTED_EDGE('',*,*,#6463,.F.);
#3538=ORIENTED_EDGE('',*,*,#6536,.T.);
#3539=ORIENTED_EDGE('',*,*,#6249,.T.);
#3540=ORIENTED_EDGE('',*,*,#6536,.F.);
#3541=ORIENTED_EDGE('',*,*,#6462,.F.);
#3542=ORIENTED_EDGE('',*,*,#6537,.T.);
#3543=ORIENTED_EDGE('',*,*,#6250,.T.);
#3544=ORIENTED_EDGE('',*,*,#6537,.F.);
#3545=ORIENTED_EDGE('',*,*,#6461,.F.);
#3546=ORIENTED_EDGE('',*,*,#6538,.T.);
#3547=ORIENTED_EDGE('',*,*,#6251,.T.);
#3548=ORIENTED_EDGE('',*,*,#6538,.F.);
#3549=ORIENTED_EDGE('',*,*,#6460,.F.);
#3550=ORIENTED_EDGE('',*,*,#6539,.T.);
#3551=ORIENTED_EDGE('',*,*,#6252,.T.);
#3552=ORIENTED_EDGE('',*,*,#6539,.F.);
#3553=ORIENTED_EDGE('',*,*,#6459,.F.);
#3554=ORIENTED_EDGE('',*,*,#6540,.T.);
#3555=ORIENTED_EDGE('',*,*,#6253,.T.);
#3556=ORIENTED_EDGE('',*,*,#6540,.F.);
#3557=ORIENTED_EDGE('',*,*,#6458,.F.);
#3558=ORIENTED_EDGE('',*,*,#6541,.T.);
#3559=ORIENTED_EDGE('',*,*,#6254,.T.);
#3560=ORIENTED_EDGE('',*,*,#6541,.F.);
#3561=ORIENTED_EDGE('',*,*,#6457,.F.);
#3562=ORIENTED_EDGE('',*,*,#6542,.T.);
#3563=ORIENTED_EDGE('',*,*,#6255,.T.);
#3564=ORIENTED_EDGE('',*,*,#6542,.F.);
#3565=ORIENTED_EDGE('',*,*,#6456,.F.);
#3566=ORIENTED_EDGE('',*,*,#6543,.T.);
#3567=ORIENTED_EDGE('',*,*,#6256,.T.);
#3568=ORIENTED_EDGE('',*,*,#6543,.F.);
#3569=ORIENTED_EDGE('',*,*,#6455,.F.);
#3570=ORIENTED_EDGE('',*,*,#6544,.T.);
#3571=ORIENTED_EDGE('',*,*,#6257,.T.);
#3572=ORIENTED_EDGE('',*,*,#6544,.F.);
#3573=ORIENTED_EDGE('',*,*,#6454,.F.);
#3574=ORIENTED_EDGE('',*,*,#6545,.T.);
#3575=ORIENTED_EDGE('',*,*,#6258,.T.);
#3576=ORIENTED_EDGE('',*,*,#6545,.F.);
#3577=ORIENTED_EDGE('',*,*,#6453,.F.);
#3578=ORIENTED_EDGE('',*,*,#6546,.T.);
#3579=ORIENTED_EDGE('',*,*,#6259,.T.);
#3580=ORIENTED_EDGE('',*,*,#6546,.F.);
#3581=ORIENTED_EDGE('',*,*,#6452,.F.);
#3582=ORIENTED_EDGE('',*,*,#6547,.T.);
#3583=ORIENTED_EDGE('',*,*,#6260,.T.);
#3584=ORIENTED_EDGE('',*,*,#6547,.F.);
#3585=ORIENTED_EDGE('',*,*,#6451,.F.);
#3586=ORIENTED_EDGE('',*,*,#6548,.T.);
#3587=ORIENTED_EDGE('',*,*,#6261,.T.);
#3588=ORIENTED_EDGE('',*,*,#6548,.F.);
#3589=ORIENTED_EDGE('',*,*,#6450,.F.);
#3590=ORIENTED_EDGE('',*,*,#6549,.T.);
#3591=ORIENTED_EDGE('',*,*,#6262,.T.);
#3592=ORIENTED_EDGE('',*,*,#6549,.F.);
#3593=ORIENTED_EDGE('',*,*,#6449,.F.);
#3594=ORIENTED_EDGE('',*,*,#6550,.T.);
#3595=ORIENTED_EDGE('',*,*,#6263,.T.);
#3596=ORIENTED_EDGE('',*,*,#6550,.F.);
#3597=ORIENTED_EDGE('',*,*,#6448,.F.);
#3598=ORIENTED_EDGE('',*,*,#6551,.T.);
#3599=ORIENTED_EDGE('',*,*,#6264,.T.);
#3600=ORIENTED_EDGE('',*,*,#6551,.F.);
#3601=ORIENTED_EDGE('',*,*,#6447,.F.);
#3602=ORIENTED_EDGE('',*,*,#6552,.T.);
#3603=ORIENTED_EDGE('',*,*,#6265,.T.);
#3604=ORIENTED_EDGE('',*,*,#6552,.F.);
#3605=ORIENTED_EDGE('',*,*,#6446,.F.);
#3606=ORIENTED_EDGE('',*,*,#6553,.T.);
#3607=ORIENTED_EDGE('',*,*,#6266,.T.);
#3608=ORIENTED_EDGE('',*,*,#6553,.F.);
#3609=ORIENTED_EDGE('',*,*,#6445,.F.);
#3610=ORIENTED_EDGE('',*,*,#6554,.T.);
#3611=ORIENTED_EDGE('',*,*,#6267,.T.);
#3612=ORIENTED_EDGE('',*,*,#6554,.F.);
#3613=ORIENTED_EDGE('',*,*,#6444,.F.);
#3614=ORIENTED_EDGE('',*,*,#6555,.T.);
#3615=ORIENTED_EDGE('',*,*,#6268,.T.);
#3616=ORIENTED_EDGE('',*,*,#6555,.F.);
#3617=ORIENTED_EDGE('',*,*,#6443,.F.);
#3618=ORIENTED_EDGE('',*,*,#6556,.T.);
#3619=ORIENTED_EDGE('',*,*,#6269,.T.);
#3620=ORIENTED_EDGE('',*,*,#6556,.F.);
#3621=ORIENTED_EDGE('',*,*,#6442,.F.);
#3622=ORIENTED_EDGE('',*,*,#6557,.T.);
#3623=ORIENTED_EDGE('',*,*,#6270,.T.);
#3624=ORIENTED_EDGE('',*,*,#6557,.F.);
#3625=ORIENTED_EDGE('',*,*,#6441,.F.);
#3626=ORIENTED_EDGE('',*,*,#6558,.T.);
#3627=ORIENTED_EDGE('',*,*,#6271,.T.);
#3628=ORIENTED_EDGE('',*,*,#6558,.F.);
#3629=ORIENTED_EDGE('',*,*,#6440,.F.);
#3630=ORIENTED_EDGE('',*,*,#6559,.T.);
#3631=ORIENTED_EDGE('',*,*,#6272,.T.);
#3632=ORIENTED_EDGE('',*,*,#6559,.F.);
#3633=ORIENTED_EDGE('',*,*,#6439,.F.);
#3634=ORIENTED_EDGE('',*,*,#6560,.T.);
#3635=ORIENTED_EDGE('',*,*,#6273,.T.);
#3636=ORIENTED_EDGE('',*,*,#6560,.F.);
#3637=ORIENTED_EDGE('',*,*,#6438,.F.);
#3638=ORIENTED_EDGE('',*,*,#6561,.T.);
#3639=ORIENTED_EDGE('',*,*,#6274,.T.);
#3640=ORIENTED_EDGE('',*,*,#6561,.F.);
#3641=ORIENTED_EDGE('',*,*,#6437,.F.);
#3642=ORIENTED_EDGE('',*,*,#6562,.T.);
#3643=ORIENTED_EDGE('',*,*,#6275,.T.);
#3644=ORIENTED_EDGE('',*,*,#6562,.F.);
#3645=ORIENTED_EDGE('',*,*,#6436,.F.);
#3646=ORIENTED_EDGE('',*,*,#6563,.T.);
#3647=ORIENTED_EDGE('',*,*,#6276,.T.);
#3648=ORIENTED_EDGE('',*,*,#6563,.F.);
#3649=ORIENTED_EDGE('',*,*,#6435,.F.);
#3650=ORIENTED_EDGE('',*,*,#6564,.T.);
#3651=ORIENTED_EDGE('',*,*,#6277,.T.);
#3652=ORIENTED_EDGE('',*,*,#6564,.F.);
#3653=ORIENTED_EDGE('',*,*,#6434,.F.);
#3654=ORIENTED_EDGE('',*,*,#6565,.T.);
#3655=ORIENTED_EDGE('',*,*,#6278,.T.);
#3656=ORIENTED_EDGE('',*,*,#6565,.F.);
#3657=ORIENTED_EDGE('',*,*,#6433,.F.);
#3658=ORIENTED_EDGE('',*,*,#6566,.T.);
#3659=ORIENTED_EDGE('',*,*,#6279,.T.);
#3660=ORIENTED_EDGE('',*,*,#6566,.F.);
#3661=ORIENTED_EDGE('',*,*,#6432,.F.);
#3662=ORIENTED_EDGE('',*,*,#6567,.T.);
#3663=ORIENTED_EDGE('',*,*,#6280,.T.);
#3664=ORIENTED_EDGE('',*,*,#6567,.F.);
#3665=ORIENTED_EDGE('',*,*,#6431,.F.);
#3666=ORIENTED_EDGE('',*,*,#6568,.T.);
#3667=ORIENTED_EDGE('',*,*,#6281,.T.);
#3668=ORIENTED_EDGE('',*,*,#6568,.F.);
#3669=ORIENTED_EDGE('',*,*,#6430,.F.);
#3670=ORIENTED_EDGE('',*,*,#6569,.T.);
#3671=ORIENTED_EDGE('',*,*,#6282,.T.);
#3672=ORIENTED_EDGE('',*,*,#6569,.F.);
#3673=ORIENTED_EDGE('',*,*,#6429,.F.);
#3674=ORIENTED_EDGE('',*,*,#6570,.T.);
#3675=ORIENTED_EDGE('',*,*,#6283,.T.);
#3676=ORIENTED_EDGE('',*,*,#6570,.F.);
#3677=ORIENTED_EDGE('',*,*,#6428,.F.);
#3678=ORIENTED_EDGE('',*,*,#6571,.T.);
#3679=ORIENTED_EDGE('',*,*,#6284,.T.);
#3680=ORIENTED_EDGE('',*,*,#6571,.F.);
#3681=ORIENTED_EDGE('',*,*,#6427,.F.);
#3682=ORIENTED_EDGE('',*,*,#6572,.T.);
#3683=ORIENTED_EDGE('',*,*,#6285,.T.);
#3684=ORIENTED_EDGE('',*,*,#6572,.F.);
#3685=ORIENTED_EDGE('',*,*,#6426,.F.);
#3686=ORIENTED_EDGE('',*,*,#6573,.T.);
#3687=ORIENTED_EDGE('',*,*,#6286,.T.);
#3688=ORIENTED_EDGE('',*,*,#6573,.F.);
#3689=ORIENTED_EDGE('',*,*,#6425,.F.);
#3690=ORIENTED_EDGE('',*,*,#6574,.T.);
#3691=ORIENTED_EDGE('',*,*,#6287,.T.);
#3692=ORIENTED_EDGE('',*,*,#6574,.F.);
#3693=ORIENTED_EDGE('',*,*,#6424,.F.);
#3694=ORIENTED_EDGE('',*,*,#6575,.T.);
#3695=ORIENTED_EDGE('',*,*,#6288,.T.);
#3696=ORIENTED_EDGE('',*,*,#6575,.F.);
#3697=ORIENTED_EDGE('',*,*,#6423,.F.);
#3698=ORIENTED_EDGE('',*,*,#6576,.T.);
#3699=ORIENTED_EDGE('',*,*,#6289,.T.);
#3700=ORIENTED_EDGE('',*,*,#6576,.F.);
#3701=ORIENTED_EDGE('',*,*,#6422,.F.);
#3702=ORIENTED_EDGE('',*,*,#6577,.T.);
#3703=ORIENTED_EDGE('',*,*,#6290,.T.);
#3704=ORIENTED_EDGE('',*,*,#6577,.F.);
#3705=ORIENTED_EDGE('',*,*,#6421,.F.);
#3706=ORIENTED_EDGE('',*,*,#6578,.T.);
#3707=ORIENTED_EDGE('',*,*,#6291,.T.);
#3708=ORIENTED_EDGE('',*,*,#6578,.F.);
#3709=ORIENTED_EDGE('',*,*,#6420,.F.);
#3710=ORIENTED_EDGE('',*,*,#6579,.T.);
#3711=ORIENTED_EDGE('',*,*,#6292,.T.);
#3712=ORIENTED_EDGE('',*,*,#6579,.F.);
#3713=ORIENTED_EDGE('',*,*,#6419,.F.);
#3714=ORIENTED_EDGE('',*,*,#6580,.T.);
#3715=ORIENTED_EDGE('',*,*,#6293,.T.);
#3716=ORIENTED_EDGE('',*,*,#6580,.F.);
#3717=ORIENTED_EDGE('',*,*,#6418,.F.);
#3718=ORIENTED_EDGE('',*,*,#6581,.T.);
#3719=ORIENTED_EDGE('',*,*,#6294,.T.);
#3720=ORIENTED_EDGE('',*,*,#6581,.F.);
#3721=ORIENTED_EDGE('',*,*,#6417,.F.);
#3722=ORIENTED_EDGE('',*,*,#6582,.T.);
#3723=ORIENTED_EDGE('',*,*,#6295,.T.);
#3724=ORIENTED_EDGE('',*,*,#6582,.F.);
#3725=ORIENTED_EDGE('',*,*,#6416,.F.);
#3726=ORIENTED_EDGE('',*,*,#6583,.T.);
#3727=ORIENTED_EDGE('',*,*,#6296,.T.);
#3728=ORIENTED_EDGE('',*,*,#6583,.F.);
#3729=ORIENTED_EDGE('',*,*,#6415,.F.);
#3730=ORIENTED_EDGE('',*,*,#6584,.T.);
#3731=ORIENTED_EDGE('',*,*,#6297,.T.);
#3732=ORIENTED_EDGE('',*,*,#6584,.F.);
#3733=ORIENTED_EDGE('',*,*,#6414,.F.);
#3734=ORIENTED_EDGE('',*,*,#6585,.T.);
#3735=ORIENTED_EDGE('',*,*,#6298,.T.);
#3736=ORIENTED_EDGE('',*,*,#6585,.F.);
#3737=ORIENTED_EDGE('',*,*,#6413,.F.);
#3738=ORIENTED_EDGE('',*,*,#6586,.T.);
#3739=ORIENTED_EDGE('',*,*,#6299,.T.);
#3740=ORIENTED_EDGE('',*,*,#6586,.F.);
#3741=ORIENTED_EDGE('',*,*,#6412,.F.);
#3742=ORIENTED_EDGE('',*,*,#6587,.T.);
#3743=ORIENTED_EDGE('',*,*,#6300,.T.);
#3744=ORIENTED_EDGE('',*,*,#6587,.F.);
#3745=ORIENTED_EDGE('',*,*,#6411,.F.);
#3746=ORIENTED_EDGE('',*,*,#6588,.T.);
#3747=ORIENTED_EDGE('',*,*,#6301,.T.);
#3748=ORIENTED_EDGE('',*,*,#6588,.F.);
#3749=ORIENTED_EDGE('',*,*,#6410,.F.);
#3750=ORIENTED_EDGE('',*,*,#6589,.T.);
#3751=ORIENTED_EDGE('',*,*,#6302,.T.);
#3752=ORIENTED_EDGE('',*,*,#6589,.F.);
#3753=ORIENTED_EDGE('',*,*,#6409,.F.);
#3754=ORIENTED_EDGE('',*,*,#6590,.T.);
#3755=ORIENTED_EDGE('',*,*,#6303,.T.);
#3756=ORIENTED_EDGE('',*,*,#6590,.F.);
#3757=ORIENTED_EDGE('',*,*,#6408,.F.);
#3758=ORIENTED_EDGE('',*,*,#6591,.T.);
#3759=ORIENTED_EDGE('',*,*,#6304,.T.);
#3760=ORIENTED_EDGE('',*,*,#6591,.F.);
#3761=ORIENTED_EDGE('',*,*,#6407,.F.);
#3762=ORIENTED_EDGE('',*,*,#6592,.T.);
#3763=ORIENTED_EDGE('',*,*,#6305,.T.);
#3764=ORIENTED_EDGE('',*,*,#6592,.F.);
#3765=ORIENTED_EDGE('',*,*,#6406,.F.);
#3766=ORIENTED_EDGE('',*,*,#6593,.T.);
#3767=ORIENTED_EDGE('',*,*,#6306,.T.);
#3768=ORIENTED_EDGE('',*,*,#6593,.F.);
#3769=ORIENTED_EDGE('',*,*,#6405,.F.);
#3770=ORIENTED_EDGE('',*,*,#6594,.T.);
#3771=ORIENTED_EDGE('',*,*,#6307,.T.);
#3772=ORIENTED_EDGE('',*,*,#6594,.F.);
#3773=ORIENTED_EDGE('',*,*,#6404,.F.);
#3774=ORIENTED_EDGE('',*,*,#6595,.T.);
#3775=ORIENTED_EDGE('',*,*,#6308,.T.);
#3776=ORIENTED_EDGE('',*,*,#6595,.F.);
#3777=ORIENTED_EDGE('',*,*,#6403,.F.);
#3778=ORIENTED_EDGE('',*,*,#6596,.T.);
#3779=ORIENTED_EDGE('',*,*,#6309,.T.);
#3780=ORIENTED_EDGE('',*,*,#6596,.F.);
#3781=ORIENTED_EDGE('',*,*,#6402,.F.);
#3782=ORIENTED_EDGE('',*,*,#6597,.T.);
#3783=ORIENTED_EDGE('',*,*,#6310,.T.);
#3784=ORIENTED_EDGE('',*,*,#6597,.F.);
#3785=ORIENTED_EDGE('',*,*,#6401,.F.);
#3786=ORIENTED_EDGE('',*,*,#6598,.T.);
#3787=ORIENTED_EDGE('',*,*,#6311,.T.);
#3788=ORIENTED_EDGE('',*,*,#6598,.F.);
#3789=ORIENTED_EDGE('',*,*,#6400,.F.);
#3790=ORIENTED_EDGE('',*,*,#6599,.T.);
#3791=ORIENTED_EDGE('',*,*,#6312,.T.);
#3792=ORIENTED_EDGE('',*,*,#6599,.F.);
#3793=ORIENTED_EDGE('',*,*,#6399,.F.);
#3794=ORIENTED_EDGE('',*,*,#6600,.T.);
#3795=ORIENTED_EDGE('',*,*,#6313,.T.);
#3796=ORIENTED_EDGE('',*,*,#6600,.F.);
#3797=ORIENTED_EDGE('',*,*,#6398,.F.);
#3798=ORIENTED_EDGE('',*,*,#6601,.T.);
#3799=ORIENTED_EDGE('',*,*,#6314,.T.);
#3800=ORIENTED_EDGE('',*,*,#6601,.F.);
#3801=ORIENTED_EDGE('',*,*,#6397,.F.);
#3802=ORIENTED_EDGE('',*,*,#6602,.T.);
#3803=ORIENTED_EDGE('',*,*,#6315,.T.);
#3804=ORIENTED_EDGE('',*,*,#6602,.F.);
#3805=ORIENTED_EDGE('',*,*,#6396,.F.);
#3806=ORIENTED_EDGE('',*,*,#6603,.T.);
#3807=ORIENTED_EDGE('',*,*,#6316,.T.);
#3808=ORIENTED_EDGE('',*,*,#6603,.F.);
#3809=ORIENTED_EDGE('',*,*,#6395,.F.);
#3810=ORIENTED_EDGE('',*,*,#6604,.T.);
#3811=ORIENTED_EDGE('',*,*,#6317,.T.);
#3812=ORIENTED_EDGE('',*,*,#6604,.F.);
#3813=ORIENTED_EDGE('',*,*,#6394,.F.);
#3814=ORIENTED_EDGE('',*,*,#6605,.T.);
#3815=ORIENTED_EDGE('',*,*,#6318,.T.);
#3816=ORIENTED_EDGE('',*,*,#6605,.F.);
#3817=ORIENTED_EDGE('',*,*,#6393,.F.);
#3818=ORIENTED_EDGE('',*,*,#6606,.T.);
#3819=ORIENTED_EDGE('',*,*,#6319,.T.);
#3820=ORIENTED_EDGE('',*,*,#6606,.F.);
#3821=ORIENTED_EDGE('',*,*,#6392,.F.);
#3822=ORIENTED_EDGE('',*,*,#6607,.T.);
#3823=ORIENTED_EDGE('',*,*,#6320,.T.);
#3824=ORIENTED_EDGE('',*,*,#6607,.F.);
#3825=ORIENTED_EDGE('',*,*,#6391,.F.);
#3826=ORIENTED_EDGE('',*,*,#6608,.T.);
#3827=ORIENTED_EDGE('',*,*,#6321,.T.);
#3828=ORIENTED_EDGE('',*,*,#6608,.F.);
#3829=ORIENTED_EDGE('',*,*,#6390,.F.);
#3830=ORIENTED_EDGE('',*,*,#6609,.T.);
#3831=ORIENTED_EDGE('',*,*,#6322,.T.);
#3832=ORIENTED_EDGE('',*,*,#6609,.F.);
#3833=ORIENTED_EDGE('',*,*,#6389,.F.);
#3834=ORIENTED_EDGE('',*,*,#6610,.T.);
#3835=ORIENTED_EDGE('',*,*,#6323,.T.);
#3836=ORIENTED_EDGE('',*,*,#6610,.F.);
#3837=ORIENTED_EDGE('',*,*,#6388,.F.);
#3838=ORIENTED_EDGE('',*,*,#6611,.T.);
#3839=ORIENTED_EDGE('',*,*,#6324,.T.);
#3840=ORIENTED_EDGE('',*,*,#6611,.F.);
#3841=ORIENTED_EDGE('',*,*,#6387,.F.);
#3842=ORIENTED_EDGE('',*,*,#6612,.T.);
#3843=ORIENTED_EDGE('',*,*,#6325,.T.);
#3844=ORIENTED_EDGE('',*,*,#6612,.F.);
#3845=ORIENTED_EDGE('',*,*,#6386,.F.);
#3846=ORIENTED_EDGE('',*,*,#6613,.T.);
#3847=ORIENTED_EDGE('',*,*,#6326,.T.);
#3848=ORIENTED_EDGE('',*,*,#6613,.F.);
#3849=ORIENTED_EDGE('',*,*,#6385,.F.);
#3850=ORIENTED_EDGE('',*,*,#6614,.T.);
#3851=ORIENTED_EDGE('',*,*,#6327,.T.);
#3852=ORIENTED_EDGE('',*,*,#6614,.F.);
#3853=ORIENTED_EDGE('',*,*,#6384,.F.);
#3854=ORIENTED_EDGE('',*,*,#6615,.T.);
#3855=ORIENTED_EDGE('',*,*,#6328,.T.);
#3856=ORIENTED_EDGE('',*,*,#6615,.F.);
#3857=ORIENTED_EDGE('',*,*,#6383,.F.);
#3858=ORIENTED_EDGE('',*,*,#6616,.T.);
#3859=ORIENTED_EDGE('',*,*,#6329,.T.);
#3860=ORIENTED_EDGE('',*,*,#6616,.F.);
#3861=ORIENTED_EDGE('',*,*,#6382,.F.);
#3862=ORIENTED_EDGE('',*,*,#6617,.T.);
#3863=ORIENTED_EDGE('',*,*,#6330,.T.);
#3864=ORIENTED_EDGE('',*,*,#6617,.F.);
#3865=ORIENTED_EDGE('',*,*,#6381,.F.);
#3866=ORIENTED_EDGE('',*,*,#6618,.T.);
#3867=ORIENTED_EDGE('',*,*,#6331,.T.);
#3868=ORIENTED_EDGE('',*,*,#6618,.F.);
#3869=ORIENTED_EDGE('',*,*,#6380,.F.);
#3870=ORIENTED_EDGE('',*,*,#6619,.T.);
#3871=ORIENTED_EDGE('',*,*,#6332,.T.);
#3872=ORIENTED_EDGE('',*,*,#6619,.F.);
#3873=ORIENTED_EDGE('',*,*,#6379,.F.);
#3874=ORIENTED_EDGE('',*,*,#6620,.T.);
#3875=ORIENTED_EDGE('',*,*,#6333,.T.);
#3876=ORIENTED_EDGE('',*,*,#6620,.F.);
#3877=ORIENTED_EDGE('',*,*,#6378,.F.);
#3878=ORIENTED_EDGE('',*,*,#6621,.T.);
#3879=ORIENTED_EDGE('',*,*,#6334,.T.);
#3880=ORIENTED_EDGE('',*,*,#6621,.F.);
#3881=ORIENTED_EDGE('',*,*,#6377,.F.);
#3882=ORIENTED_EDGE('',*,*,#6622,.T.);
#3883=ORIENTED_EDGE('',*,*,#6335,.T.);
#3884=ORIENTED_EDGE('',*,*,#6622,.F.);
#3885=ORIENTED_EDGE('',*,*,#6376,.F.);
#3886=ORIENTED_EDGE('',*,*,#6623,.T.);
#3887=ORIENTED_EDGE('',*,*,#6336,.T.);
#3888=ORIENTED_EDGE('',*,*,#6623,.F.);
#3889=ORIENTED_EDGE('',*,*,#6375,.F.);
#3890=ORIENTED_EDGE('',*,*,#6624,.T.);
#3891=ORIENTED_EDGE('',*,*,#6337,.T.);
#3892=ORIENTED_EDGE('',*,*,#6624,.F.);
#3893=ORIENTED_EDGE('',*,*,#6374,.F.);
#3894=ORIENTED_EDGE('',*,*,#6625,.T.);
#3895=ORIENTED_EDGE('',*,*,#6338,.T.);
#3896=ORIENTED_EDGE('',*,*,#6625,.F.);
#3897=ORIENTED_EDGE('',*,*,#6373,.F.);
#3898=ORIENTED_EDGE('',*,*,#6626,.T.);
#3899=ORIENTED_EDGE('',*,*,#6339,.T.);
#3900=ORIENTED_EDGE('',*,*,#6626,.F.);
#3901=ORIENTED_EDGE('',*,*,#6372,.F.);
#3902=ORIENTED_EDGE('',*,*,#6627,.T.);
#3903=ORIENTED_EDGE('',*,*,#6340,.T.);
#3904=ORIENTED_EDGE('',*,*,#6627,.F.);
#3905=ORIENTED_EDGE('',*,*,#6371,.F.);
#3906=ORIENTED_EDGE('',*,*,#6628,.T.);
#3907=ORIENTED_EDGE('',*,*,#6341,.T.);
#3908=ORIENTED_EDGE('',*,*,#6628,.F.);
#3909=ORIENTED_EDGE('',*,*,#6370,.F.);
#3910=ORIENTED_EDGE('',*,*,#6629,.T.);
#3911=ORIENTED_EDGE('',*,*,#6342,.T.);
#3912=ORIENTED_EDGE('',*,*,#6629,.F.);
#3913=ORIENTED_EDGE('',*,*,#6369,.F.);
#3914=ORIENTED_EDGE('',*,*,#6630,.T.);
#3915=ORIENTED_EDGE('',*,*,#6343,.T.);
#3916=ORIENTED_EDGE('',*,*,#6630,.F.);
#3917=ORIENTED_EDGE('',*,*,#6368,.F.);
#3918=ORIENTED_EDGE('',*,*,#6631,.T.);
#3919=ORIENTED_EDGE('',*,*,#6344,.T.);
#3920=ORIENTED_EDGE('',*,*,#6631,.F.);
#3921=ORIENTED_EDGE('',*,*,#6367,.F.);
#3922=ORIENTED_EDGE('',*,*,#6632,.T.);
#3923=ORIENTED_EDGE('',*,*,#6345,.T.);
#3924=ORIENTED_EDGE('',*,*,#6632,.F.);
#3925=ORIENTED_EDGE('',*,*,#6366,.F.);
#3926=ORIENTED_EDGE('',*,*,#6633,.T.);
#3927=ORIENTED_EDGE('',*,*,#6346,.T.);
#3928=ORIENTED_EDGE('',*,*,#6633,.F.);
#3929=ORIENTED_EDGE('',*,*,#6365,.F.);
#3930=ORIENTED_EDGE('',*,*,#6634,.T.);
#3931=ORIENTED_EDGE('',*,*,#6347,.T.);
#3932=ORIENTED_EDGE('',*,*,#6634,.F.);
#3933=ORIENTED_EDGE('',*,*,#6364,.F.);
#3934=ORIENTED_EDGE('',*,*,#6635,.T.);
#3935=ORIENTED_EDGE('',*,*,#6348,.T.);
#3936=ORIENTED_EDGE('',*,*,#6635,.F.);
#3937=ORIENTED_EDGE('',*,*,#6363,.F.);
#3938=ORIENTED_EDGE('',*,*,#6636,.T.);
#3939=ORIENTED_EDGE('',*,*,#6349,.T.);
#3940=ORIENTED_EDGE('',*,*,#6636,.F.);
#3941=ORIENTED_EDGE('',*,*,#6362,.F.);
#3942=ORIENTED_EDGE('',*,*,#6637,.T.);
#3943=ORIENTED_EDGE('',*,*,#6350,.T.);
#3944=ORIENTED_EDGE('',*,*,#6637,.F.);
#3945=ORIENTED_EDGE('',*,*,#6361,.F.);
#3946=ORIENTED_EDGE('',*,*,#6638,.T.);
#3947=ORIENTED_EDGE('',*,*,#6351,.T.);
#3948=ORIENTED_EDGE('',*,*,#6638,.F.);
#3949=ORIENTED_EDGE('',*,*,#6360,.F.);
#3950=ORIENTED_EDGE('',*,*,#6639,.T.);
#3951=ORIENTED_EDGE('',*,*,#6352,.T.);
#3952=ORIENTED_EDGE('',*,*,#6639,.F.);
#3953=ORIENTED_EDGE('',*,*,#6359,.F.);
#3954=ORIENTED_EDGE('',*,*,#6640,.T.);
#3955=ORIENTED_EDGE('',*,*,#6353,.T.);
#3956=ORIENTED_EDGE('',*,*,#6640,.F.);
#3957=ORIENTED_EDGE('',*,*,#6358,.F.);
#3958=ORIENTED_EDGE('',*,*,#6641,.T.);
#3959=ORIENTED_EDGE('',*,*,#6354,.T.);
#3960=ORIENTED_EDGE('',*,*,#6641,.F.);
#3961=ORIENTED_EDGE('',*,*,#6357,.F.);
#3962=ORIENTED_EDGE('',*,*,#6642,.T.);
#3963=ORIENTED_EDGE('',*,*,#6212,.T.);
#3964=ORIENTED_EDGE('',*,*,#6642,.F.);
#3965=ORIENTED_EDGE('',*,*,#6356,.F.);
#3966=ORIENTED_EDGE('',*,*,#6500,.T.);
#3967=ORIENTED_EDGE('',*,*,#6183,.T.);
#3968=ORIENTED_EDGE('',*,*,#6207,.T.);
#3969=ORIENTED_EDGE('',*,*,#6643,.F.);
#3970=ORIENTED_EDGE('',*,*,#6644,.T.);
#3971=ORIENTED_EDGE('',*,*,#6185,.T.);
#3972=ORIENTED_EDGE('',*,*,#6184,.T.);
#3973=ORIENTED_EDGE('',*,*,#6643,.T.);
#3974=ORIENTED_EDGE('',*,*,#6208,.F.);
#3975=ORIENTED_EDGE('',*,*,#6202,.F.);
#3976=ORIENTED_EDGE('',*,*,#6201,.F.);
#3977=ORIENTED_EDGE('',*,*,#6200,.F.);
#3978=ORIENTED_EDGE('',*,*,#6199,.F.);
#3979=ORIENTED_EDGE('',*,*,#6198,.F.);
#3980=ORIENTED_EDGE('',*,*,#6197,.F.);
#3981=ORIENTED_EDGE('',*,*,#6196,.F.);
#3982=ORIENTED_EDGE('',*,*,#6195,.F.);
#3983=ORIENTED_EDGE('',*,*,#6210,.F.);
#3984=ORIENTED_EDGE('',*,*,#6209,.F.);
#3985=ORIENTED_EDGE('',*,*,#6190,.T.);
#3986=ORIENTED_EDGE('',*,*,#6189,.T.);
#3987=ORIENTED_EDGE('',*,*,#6188,.T.);
#3988=ORIENTED_EDGE('',*,*,#6187,.T.);
#3989=ORIENTED_EDGE('',*,*,#6186,.T.);
#3990=ORIENTED_EDGE('',*,*,#6499,.T.);
#3991=ORIENTED_EDGE('',*,*,#6644,.F.);
#3992=ORIENTED_EDGE('',*,*,#6355,.T.);
#3993=ORIENTED_EDGE('',*,*,#6645,.T.);
#3994=ORIENTED_EDGE('',*,*,#6181,.T.);
#3995=ORIENTED_EDGE('',*,*,#6646,.T.);
#3996=ORIENTED_EDGE('',*,*,#6646,.F.);
#3997=ORIENTED_EDGE('',*,*,#6211,.F.);
#3998=ORIENTED_EDGE('',*,*,#6645,.F.);
#3999=ORIENTED_EDGE('',*,*,#6182,.T.);
#6181=EDGE_CURVE('',#7867,#7867,#643,.T.);
#6182=EDGE_CURVE('',#7868,#7868,#644,.T.);
#6183=EDGE_CURVE('',#7869,#7870,#1109,.T.);
#6184=EDGE_CURVE('',#7871,#7869,#1894,.T.);
#6185=EDGE_CURVE('',#7872,#7871,#1895,.T.);
#6186=EDGE_CURVE('',#7873,#7872,#1896,.T.);
#6187=EDGE_CURVE('',#7874,#7873,#1897,.T.);
#6188=EDGE_CURVE('',#7875,#7874,#1898,.T.);
#6189=EDGE_CURVE('',#7876,#7875,#1899,.T.);
#6190=EDGE_CURVE('',#7877,#7876,#1900,.T.);
#6191=EDGE_CURVE('',#7878,#7877,#8903,.T.);
#6192=EDGE_CURVE('',#7878,#7879,#1901,.T.);
#6193=EDGE_CURVE('',#7870,#7879,#8904,.T.);
#6194=EDGE_CURVE('',#7880,#7881,#8905,.T.);
#6195=EDGE_CURVE('',#7880,#7882,#1902,.T.);
#6196=EDGE_CURVE('',#7882,#7883,#1903,.T.);
#6197=EDGE_CURVE('',#7883,#7884,#1904,.T.);
#6198=EDGE_CURVE('',#7884,#7885,#1905,.T.);
#6199=EDGE_CURVE('',#7885,#7886,#1906,.T.);
#6200=EDGE_CURVE('',#7886,#7887,#1907,.T.);
#6201=EDGE_CURVE('',#7887,#7888,#1908,.T.);
#6202=EDGE_CURVE('',#7888,#7889,#1909,.T.);
#6203=EDGE_CURVE('',#7890,#7889,#8906,.T.);
#6204=EDGE_CURVE('',#7881,#7890,#1910,.T.);
#6205=EDGE_CURVE('',#7881,#7878,#8907,.T.);
#6206=EDGE_CURVE('',#7879,#7890,#8908,.T.);
#6207=EDGE_CURVE('',#7870,#7891,#8909,.T.);
#6208=EDGE_CURVE('',#7889,#7891,#8910,.T.);
#6209=EDGE_CURVE('',#7877,#7880,#8911,.T.);
#6210=EDGE_CURVE('',#7880,#7880,#645,.T.);
#6211=EDGE_CURVE('',#7892,#7892,#646,.T.);
#6212=EDGE_CURVE('',#7893,#7894,#8912,.T.);
#6213=EDGE_CURVE('',#7895,#7893,#647,.T.);
#6214=EDGE_CURVE('',#7896,#7895,#8913,.T.);
#6215=EDGE_CURVE('',#7897,#7896,#8914,.T.);
#6216=EDGE_CURVE('',#7898,#7897,#648,.T.);
#6217=EDGE_CURVE('',#7899,#7898,#8915,.T.);
#6218=EDGE_CURVE('',#7900,#7899,#8916,.T.);
#6219=EDGE_CURVE('',#7901,#7900,#649,.T.);
#6220=EDGE_CURVE('',#7902,#7901,#8917,.T.);
#6221=EDGE_CURVE('',#7903,#7902,#8918,.T.);
#6222=EDGE_CURVE('',#7904,#7903,#650,.T.);
#6223=EDGE_CURVE('',#7905,#7904,#8919,.T.);
#6224=EDGE_CURVE('',#7906,#7905,#8920,.T.);
#6225=EDGE_CURVE('',#7907,#7906,#651,.T.);
#6226=EDGE_CURVE('',#7908,#7907,#8921,.T.);
#6227=EDGE_CURVE('',#7909,#7908,#8922,.T.);
#6228=EDGE_CURVE('',#7910,#7909,#652,.T.);
#6229=EDGE_CURVE('',#7911,#7910,#8923,.T.);
#6230=EDGE_CURVE('',#7912,#7911,#8924,.T.);
#6231=EDGE_CURVE('',#7913,#7912,#653,.T.);
#6232=EDGE_CURVE('',#7914,#7913,#8925,.T.);
#6233=EDGE_CURVE('',#7915,#7914,#8926,.T.);
#6234=EDGE_CURVE('',#7916,#7915,#654,.T.);
#6235=EDGE_CURVE('',#7917,#7916,#8927,.T.);
#6236=EDGE_CURVE('',#7918,#7917,#8928,.T.);
#6237=EDGE_CURVE('',#7919,#7918,#655,.T.);
#6238=EDGE_CURVE('',#7920,#7919,#8929,.T.);
#6239=EDGE_CURVE('',#7921,#7920,#8930,.T.);
#6240=EDGE_CURVE('',#7922,#7921,#656,.T.);
#6241=EDGE_CURVE('',#7923,#7922,#8931,.T.);
#6242=EDGE_CURVE('',#7924,#7923,#8932,.T.);
#6243=EDGE_CURVE('',#7925,#7924,#657,.T.);
#6244=EDGE_CURVE('',#7926,#7925,#8933,.T.);
#6245=EDGE_CURVE('',#7927,#7926,#8934,.T.);
#6246=EDGE_CURVE('',#7928,#7927,#658,.T.);
#6247=EDGE_CURVE('',#7929,#7928,#8935,.T.);
#6248=EDGE_CURVE('',#7930,#7929,#8936,.T.);
#6249=EDGE_CURVE('',#7931,#7930,#659,.T.);
#6250=EDGE_CURVE('',#7932,#7931,#8937,.T.);
#6251=EDGE_CURVE('',#7933,#7932,#8938,.T.);
#6252=EDGE_CURVE('',#7934,#7933,#660,.T.);
#6253=EDGE_CURVE('',#7935,#7934,#8939,.T.);
#6254=EDGE_CURVE('',#7936,#7935,#8940,.T.);
#6255=EDGE_CURVE('',#7937,#7936,#661,.T.);
#6256=EDGE_CURVE('',#7938,#7937,#8941,.T.);
#6257=EDGE_CURVE('',#7939,#7938,#8942,.T.);
#6258=EDGE_CURVE('',#7940,#7939,#662,.T.);
#6259=EDGE_CURVE('',#7941,#7940,#8943,.T.);
#6260=EDGE_CURVE('',#7942,#7941,#8944,.T.);
#6261=EDGE_CURVE('',#7943,#7942,#663,.T.);
#6262=EDGE_CURVE('',#7944,#7943,#8945,.T.);
#6263=EDGE_CURVE('',#7945,#7944,#8946,.T.);
#6264=EDGE_CURVE('',#7946,#7945,#664,.T.);
#6265=EDGE_CURVE('',#7947,#7946,#8947,.T.);
#6266=EDGE_CURVE('',#7948,#7947,#8948,.T.);
#6267=EDGE_CURVE('',#7949,#7948,#665,.T.);
#6268=EDGE_CURVE('',#7950,#7949,#8949,.T.);
#6269=EDGE_CURVE('',#7951,#7950,#8950,.T.);
#6270=EDGE_CURVE('',#7952,#7951,#666,.T.);
#6271=EDGE_CURVE('',#7953,#7952,#8951,.T.);
#6272=EDGE_CURVE('',#7954,#7953,#8952,.T.);
#6273=EDGE_CURVE('',#7955,#7954,#667,.T.);
#6274=EDGE_CURVE('',#7956,#7955,#8953,.T.);
#6275=EDGE_CURVE('',#7957,#7956,#8954,.T.);
#6276=EDGE_CURVE('',#7958,#7957,#668,.T.);
#6277=EDGE_CURVE('',#7959,#7958,#8955,.T.);
#6278=EDGE_CURVE('',#7960,#7959,#8956,.T.);
#6279=EDGE_CURVE('',#7961,#7960,#669,.T.);
#6280=EDGE_CURVE('',#7962,#7961,#8957,.T.);
#6281=EDGE_CURVE('',#7963,#7962,#8958,.T.);
#6282=EDGE_CURVE('',#7964,#7963,#670,.T.);
#6283=EDGE_CURVE('',#7965,#7964,#8959,.T.);
#6284=EDGE_CURVE('',#7966,#7965,#8960,.T.);
#6285=EDGE_CURVE('',#7967,#7966,#671,.T.);
#6286=EDGE_CURVE('',#7968,#7967,#8961,.T.);
#6287=EDGE_CURVE('',#7969,#7968,#8962,.T.);
#6288=EDGE_CURVE('',#7970,#7969,#672,.T.);
#6289=EDGE_CURVE('',#7971,#7970,#8963,.T.);
#6290=EDGE_CURVE('',#7972,#7971,#8964,.T.);
#6291=EDGE_CURVE('',#7973,#7972,#673,.T.);
#6292=EDGE_CURVE('',#7974,#7973,#8965,.T.);
#6293=EDGE_CURVE('',#7975,#7974,#8966,.T.);
#6294=EDGE_CURVE('',#7976,#7975,#674,.T.);
#6295=EDGE_CURVE('',#7977,#7976,#8967,.T.);
#6296=EDGE_CURVE('',#7978,#7977,#8968,.T.);
#6297=EDGE_CURVE('',#7979,#7978,#675,.T.);
#6298=EDGE_CURVE('',#7980,#7979,#8969,.T.);
#6299=EDGE_CURVE('',#7981,#7980,#8970,.T.);
#6300=EDGE_CURVE('',#7982,#7981,#676,.T.);
#6301=EDGE_CURVE('',#7983,#7982,#8971,.T.);
#6302=EDGE_CURVE('',#7984,#7983,#8972,.T.);
#6303=EDGE_CURVE('',#7985,#7984,#677,.T.);
#6304=EDGE_CURVE('',#7986,#7985,#8973,.T.);
#6305=EDGE_CURVE('',#7987,#7986,#8974,.T.);
#6306=EDGE_CURVE('',#7988,#7987,#678,.T.);
#6307=EDGE_CURVE('',#7989,#7988,#8975,.T.);
#6308=EDGE_CURVE('',#7990,#7989,#8976,.T.);
#6309=EDGE_CURVE('',#7991,#7990,#679,.T.);
#6310=EDGE_CURVE('',#7992,#7991,#8977,.T.);
#6311=EDGE_CURVE('',#7993,#7992,#8978,.T.);
#6312=EDGE_CURVE('',#7994,#7993,#680,.T.);
#6313=EDGE_CURVE('',#7995,#7994,#8979,.T.);
#6314=EDGE_CURVE('',#7996,#7995,#8980,.T.);
#6315=EDGE_CURVE('',#7997,#7996,#681,.T.);
#6316=EDGE_CURVE('',#7998,#7997,#8981,.T.);
#6317=EDGE_CURVE('',#7999,#7998,#8982,.T.);
#6318=EDGE_CURVE('',#8000,#7999,#682,.T.);
#6319=EDGE_CURVE('',#8001,#8000,#8983,.T.);
#6320=EDGE_CURVE('',#8002,#8001,#8984,.T.);
#6321=EDGE_CURVE('',#8003,#8002,#683,.T.);
#6322=EDGE_CURVE('',#8004,#8003,#8985,.T.);
#6323=EDGE_CURVE('',#8005,#8004,#8986,.T.);
#6324=EDGE_CURVE('',#8006,#8005,#684,.T.);
#6325=EDGE_CURVE('',#8007,#8006,#8987,.T.);
#6326=EDGE_CURVE('',#8008,#8007,#8988,.T.);
#6327=EDGE_CURVE('',#8009,#8008,#685,.T.);
#6328=EDGE_CURVE('',#8010,#8009,#8989,.T.);
#6329=EDGE_CURVE('',#8011,#8010,#8990,.T.);
#6330=EDGE_CURVE('',#8012,#8011,#686,.T.);
#6331=EDGE_CURVE('',#8013,#8012,#8991,.T.);
#6332=EDGE_CURVE('',#8014,#8013,#8992,.T.);
#6333=EDGE_CURVE('',#8015,#8014,#687,.T.);
#6334=EDGE_CURVE('',#8016,#8015,#8993,.T.);
#6335=EDGE_CURVE('',#8017,#8016,#8994,.T.);
#6336=EDGE_CURVE('',#8018,#8017,#688,.T.);
#6337=EDGE_CURVE('',#8019,#8018,#8995,.T.);
#6338=EDGE_CURVE('',#8020,#8019,#8996,.T.);
#6339=EDGE_CURVE('',#8021,#8020,#689,.T.);
#6340=EDGE_CURVE('',#8022,#8021,#8997,.T.);
#6341=EDGE_CURVE('',#8023,#8022,#8998,.T.);
#6342=EDGE_CURVE('',#8024,#8023,#8999,.T.);
#6343=EDGE_CURVE('',#8025,#8024,#9000,.T.);
#6344=EDGE_CURVE('',#8026,#8025,#690,.T.);
#6345=EDGE_CURVE('',#8027,#8026,#9001,.T.);
#6346=EDGE_CURVE('',#8028,#8027,#9002,.T.);
#6347=EDGE_CURVE('',#8029,#8028,#691,.T.);
#6348=EDGE_CURVE('',#8030,#8029,#9003,.T.);
#6349=EDGE_CURVE('',#8031,#8030,#9004,.T.);
#6350=EDGE_CURVE('',#8032,#8031,#692,.T.);
#6351=EDGE_CURVE('',#8033,#8032,#9005,.T.);
#6352=EDGE_CURVE('',#8034,#8033,#9006,.T.);
#6353=EDGE_CURVE('',#8035,#8034,#693,.T.);
#6354=EDGE_CURVE('',#7894,#8035,#9007,.T.);
#6355=EDGE_CURVE('',#8036,#8036,#694,.T.);
#6356=EDGE_CURVE('',#8037,#8038,#9008,.T.);
#6357=EDGE_CURVE('',#8038,#8039,#9009,.T.);
#6358=EDGE_CURVE('',#8039,#8040,#695,.T.);
#6359=EDGE_CURVE('',#8040,#8041,#9010,.T.);
#6360=EDGE_CURVE('',#8041,#8042,#9011,.T.);
#6361=EDGE_CURVE('',#8042,#8043,#696,.T.);
#6362=EDGE_CURVE('',#8043,#8044,#9012,.T.);
#6363=EDGE_CURVE('',#8044,#8045,#9013,.T.);
#6364=EDGE_CURVE('',#8045,#8046,#697,.T.);
#6365=EDGE_CURVE('',#8046,#8047,#9014,.T.);
#6366=EDGE_CURVE('',#8047,#8048,#9015,.T.);
#6367=EDGE_CURVE('',#8048,#8049,#698,.T.);
#6368=EDGE_CURVE('',#8049,#8050,#9016,.T.);
#6369=EDGE_CURVE('',#8050,#8051,#9017,.T.);
#6370=EDGE_CURVE('',#8051,#8052,#9018,.T.);
#6371=EDGE_CURVE('',#8052,#8053,#9019,.T.);
#6372=EDGE_CURVE('',#8053,#8054,#699,.T.);
#6373=EDGE_CURVE('',#8054,#8055,#9020,.T.);
#6374=EDGE_CURVE('',#8055,#8056,#9021,.T.);
#6375=EDGE_CURVE('',#8056,#8057,#700,.T.);
#6376=EDGE_CURVE('',#8057,#8058,#9022,.T.);
#6377=EDGE_CURVE('',#8058,#8059,#9023,.T.);
#6378=EDGE_CURVE('',#8059,#8060,#701,.T.);
#6379=EDGE_CURVE('',#8060,#8061,#9024,.T.);
#6380=EDGE_CURVE('',#8061,#8062,#9025,.T.);
#6381=EDGE_CURVE('',#8062,#8063,#702,.T.);
#6382=EDGE_CURVE('',#8063,#8064,#9026,.T.);
#6383=EDGE_CURVE('',#8064,#8065,#9027,.T.);
#6384=EDGE_CURVE('',#8065,#8066,#703,.T.);
#6385=EDGE_CURVE('',#8066,#8067,#9028,.T.);
#6386=EDGE_CURVE('',#8067,#8068,#9029,.T.);
#6387=EDGE_CURVE('',#8068,#8069,#704,.T.);
#6388=EDGE_CURVE('',#8069,#8070,#9030,.T.);
#6389=EDGE_CURVE('',#8070,#8071,#9031,.T.);
#6390=EDGE_CURVE('',#8071,#8072,#705,.T.);
#6391=EDGE_CURVE('',#8072,#8073,#9032,.T.);
#6392=EDGE_CURVE('',#8073,#8074,#9033,.T.);
#6393=EDGE_CURVE('',#8074,#8075,#706,.T.);
#6394=EDGE_CURVE('',#8075,#8076,#9034,.T.);
#6395=EDGE_CURVE('',#8076,#8077,#9035,.T.);
#6396=EDGE_CURVE('',#8077,#8078,#707,.T.);
#6397=EDGE_CURVE('',#8078,#8079,#9036,.T.);
#6398=EDGE_CURVE('',#8079,#8080,#9037,.T.);
#6399=EDGE_CURVE('',#8080,#8081,#708,.T.);
#6400=EDGE_CURVE('',#8081,#8082,#9038,.T.);
#6401=EDGE_CURVE('',#8082,#8083,#9039,.T.);
#6402=EDGE_CURVE('',#8083,#8084,#709,.T.);
#6403=EDGE_CURVE('',#8084,#8085,#9040,.T.);
#6404=EDGE_CURVE('',#8085,#8086,#9041,.T.);
#6405=EDGE_CURVE('',#8086,#8087,#710,.T.);
#6406=EDGE_CURVE('',#8087,#8088,#9042,.T.);
#6407=EDGE_CURVE('',#8088,#8089,#9043,.T.);
#6408=EDGE_CURVE('',#8089,#8090,#711,.T.);
#6409=EDGE_CURVE('',#8090,#8091,#9044,.T.);
#6410=EDGE_CURVE('',#8091,#8092,#9045,.T.);
#6411=EDGE_CURVE('',#8092,#8093,#712,.T.);
#6412=EDGE_CURVE('',#8093,#8094,#9046,.T.);
#6413=EDGE_CURVE('',#8094,#8095,#9047,.T.);
#6414=EDGE_CURVE('',#8095,#8096,#713,.T.);
#6415=EDGE_CURVE('',#8096,#8097,#9048,.T.);
#6416=EDGE_CURVE('',#8097,#8098,#9049,.T.);
#6417=EDGE_CURVE('',#8098,#8099,#714,.T.);
#6418=EDGE_CURVE('',#8099,#8100,#9050,.T.);
#6419=EDGE_CURVE('',#8100,#8101,#9051,.T.);
#6420=EDGE_CURVE('',#8101,#8102,#715,.T.);
#6421=EDGE_CURVE('',#8102,#8103,#9052,.T.);
#6422=EDGE_CURVE('',#8103,#8104,#9053,.T.);
#6423=EDGE_CURVE('',#8104,#8105,#716,.T.);
#6424=EDGE_CURVE('',#8105,#8106,#9054,.T.);
#6425=EDGE_CURVE('',#8106,#8107,#9055,.T.);
#6426=EDGE_CURVE('',#8107,#8108,#717,.T.);
#6427=EDGE_CURVE('',#8108,#8109,#9056,.T.);
#6428=EDGE_CURVE('',#8109,#8110,#9057,.T.);
#6429=EDGE_CURVE('',#8110,#8111,#718,.T.);
#6430=EDGE_CURVE('',#8111,#8112,#9058,.T.);
#6431=EDGE_CURVE('',#8112,#8113,#9059,.T.);
#6432=EDGE_CURVE('',#8113,#8114,#719,.T.);
#6433=EDGE_CURVE('',#8114,#8115,#9060,.T.);
#6434=EDGE_CURVE('',#8115,#8116,#9061,.T.);
#6435=EDGE_CURVE('',#8116,#8117,#720,.T.);
#6436=EDGE_CURVE('',#8117,#8118,#9062,.T.);
#6437=EDGE_CURVE('',#8118,#8119,#9063,.T.);
#6438=EDGE_CURVE('',#8119,#8120,#721,.T.);
#6439=EDGE_CURVE('',#8120,#8121,#9064,.T.);
#6440=EDGE_CURVE('',#8121,#8122,#9065,.T.);
#6441=EDGE_CURVE('',#8122,#8123,#722,.T.);
#6442=EDGE_CURVE('',#8123,#8124,#9066,.T.);
#6443=EDGE_CURVE('',#8124,#8125,#9067,.T.);
#6444=EDGE_CURVE('',#8125,#8126,#723,.T.);
#6445=EDGE_CURVE('',#8126,#8127,#9068,.T.);
#6446=EDGE_CURVE('',#8127,#8128,#9069,.T.);
#6447=EDGE_CURVE('',#8128,#8129,#724,.T.);
#6448=EDGE_CURVE('',#8129,#8130,#9070,.T.);
#6449=EDGE_CURVE('',#8130,#8131,#9071,.T.);
#6450=EDGE_CURVE('',#8131,#8132,#725,.T.);
#6451=EDGE_CURVE('',#8132,#8133,#9072,.T.);
#6452=EDGE_CURVE('',#8133,#8134,#9073,.T.);
#6453=EDGE_CURVE('',#8134,#8135,#726,.T.);
#6454=EDGE_CURVE('',#8135,#8136,#9074,.T.);
#6455=EDGE_CURVE('',#8136,#8137,#9075,.T.);
#6456=EDGE_CURVE('',#8137,#8138,#727,.T.);
#6457=EDGE_CURVE('',#8138,#8139,#9076,.T.);
#6458=EDGE_CURVE('',#8139,#8140,#9077,.T.);
#6459=EDGE_CURVE('',#8140,#8141,#728,.T.);
#6460=EDGE_CURVE('',#8141,#8142,#9078,.T.);
#6461=EDGE_CURVE('',#8142,#8143,#9079,.T.);
#6462=EDGE_CURVE('',#8143,#8144,#729,.T.);
#6463=EDGE_CURVE('',#8144,#8145,#9080,.T.);
#6464=EDGE_CURVE('',#8145,#8146,#9081,.T.);
#6465=EDGE_CURVE('',#8146,#8147,#730,.T.);
#6466=EDGE_CURVE('',#8147,#8148,#9082,.T.);
#6467=EDGE_CURVE('',#8148,#8149,#9083,.T.);
#6468=EDGE_CURVE('',#8149,#8150,#731,.T.);
#6469=EDGE_CURVE('',#8150,#8151,#9084,.T.);
#6470=EDGE_CURVE('',#8151,#8152,#9085,.T.);
#6471=EDGE_CURVE('',#8152,#8153,#732,.T.);
#6472=EDGE_CURVE('',#8153,#8154,#9086,.T.);
#6473=EDGE_CURVE('',#8154,#8155,#9087,.T.);
#6474=EDGE_CURVE('',#8155,#8156,#733,.T.);
#6475=EDGE_CURVE('',#8156,#8157,#9088,.T.);
#6476=EDGE_CURVE('',#8157,#8158,#9089,.T.);
#6477=EDGE_CURVE('',#8158,#8159,#734,.T.);
#6478=EDGE_CURVE('',#8159,#8160,#9090,.T.);
#6479=EDGE_CURVE('',#8160,#8161,#9091,.T.);
#6480=EDGE_CURVE('',#8161,#8162,#735,.T.);
#6481=EDGE_CURVE('',#8162,#8163,#9092,.T.);
#6482=EDGE_CURVE('',#8163,#8164,#9093,.T.);
#6483=EDGE_CURVE('',#8164,#8165,#736,.T.);
#6484=EDGE_CURVE('',#8165,#8166,#9094,.T.);
#6485=EDGE_CURVE('',#8166,#8167,#9095,.T.);
#6486=EDGE_CURVE('',#8167,#8168,#737,.T.);
#6487=EDGE_CURVE('',#8168,#8169,#9096,.T.);
#6488=EDGE_CURVE('',#8169,#8170,#9097,.T.);
#6489=EDGE_CURVE('',#8170,#8171,#738,.T.);
#6490=EDGE_CURVE('',#8171,#8172,#9098,.T.);
#6491=EDGE_CURVE('',#8172,#8173,#9099,.T.);
#6492=EDGE_CURVE('',#8173,#8174,#739,.T.);
#6493=EDGE_CURVE('',#8174,#8175,#9100,.T.);
#6494=EDGE_CURVE('',#8175,#8176,#9101,.T.);
#6495=EDGE_CURVE('',#8176,#8177,#740,.T.);
#6496=EDGE_CURVE('',#8177,#8178,#9102,.T.);
#6497=EDGE_CURVE('',#8178,#8179,#9103,.T.);
#6498=EDGE_CURVE('',#8179,#8037,#741,.T.);
#6499=EDGE_CURVE('',#8180,#8180,#742,.T.);
#6500=EDGE_CURVE('',#8037,#7893,#9104,.T.);
#6501=EDGE_CURVE('',#8179,#7895,#9105,.T.);
#6502=EDGE_CURVE('',#8178,#7896,#9106,.T.);
#6503=EDGE_CURVE('',#8177,#7897,#9107,.T.);
#6504=EDGE_CURVE('',#8176,#7898,#9108,.T.);
#6505=EDGE_CURVE('',#8175,#7899,#9109,.T.);
#6506=EDGE_CURVE('',#8174,#7900,#9110,.T.);
#6507=EDGE_CURVE('',#8173,#7901,#9111,.T.);
#6508=EDGE_CURVE('',#8172,#7902,#9112,.T.);
#6509=EDGE_CURVE('',#8171,#7903,#9113,.T.);
#6510=EDGE_CURVE('',#8170,#7904,#9114,.T.);
#6511=EDGE_CURVE('',#8169,#7905,#9115,.T.);
#6512=EDGE_CURVE('',#8168,#7906,#9116,.T.);
#6513=EDGE_CURVE('',#8167,#7907,#9117,.T.);
#6514=EDGE_CURVE('',#8166,#7908,#9118,.T.);
#6515=EDGE_CURVE('',#8165,#7909,#9119,.T.);
#6516=EDGE_CURVE('',#8164,#7910,#9120,.T.);
#6517=EDGE_CURVE('',#8163,#7911,#9121,.T.);
#6518=EDGE_CURVE('',#8162,#7912,#9122,.T.);
#6519=EDGE_CURVE('',#8161,#7913,#9123,.T.);
#6520=EDGE_CURVE('',#8160,#7914,#9124,.T.);
#6521=EDGE_CURVE('',#8159,#7915,#9125,.T.);
#6522=EDGE_CURVE('',#8158,#7916,#9126,.T.);
#6523=EDGE_CURVE('',#8157,#7917,#9127,.T.);
#6524=EDGE_CURVE('',#8156,#7918,#9128,.T.);
#6525=EDGE_CURVE('',#8155,#7919,#9129,.T.);
#6526=EDGE_CURVE('',#8154,#7920,#9130,.T.);
#6527=EDGE_CURVE('',#8153,#7921,#9131,.T.);
#6528=EDGE_CURVE('',#8152,#7922,#9132,.T.);
#6529=EDGE_CURVE('',#8151,#7923,#9133,.T.);
#6530=EDGE_CURVE('',#8150,#7924,#9134,.T.);
#6531=EDGE_CURVE('',#8149,#7925,#9135,.T.);
#6532=EDGE_CURVE('',#8148,#7926,#9136,.T.);
#6533=EDGE_CURVE('',#8147,#7927,#9137,.T.);
#6534=EDGE_CURVE('',#8146,#7928,#9138,.T.);
#6535=EDGE_CURVE('',#8145,#7929,#9139,.T.);
#6536=EDGE_CURVE('',#8144,#7930,#9140,.T.);
#6537=EDGE_CURVE('',#8143,#7931,#9141,.T.);
#6538=EDGE_CURVE('',#8142,#7932,#9142,.T.);
#6539=EDGE_CURVE('',#8141,#7933,#9143,.T.);
#6540=EDGE_CURVE('',#8140,#7934,#9144,.T.);
#6541=EDGE_CURVE('',#8139,#7935,#9145,.T.);
#6542=EDGE_CURVE('',#8138,#7936,#9146,.T.);
#6543=EDGE_CURVE('',#8137,#7937,#9147,.T.);
#6544=EDGE_CURVE('',#8136,#7938,#9148,.T.);
#6545=EDGE_CURVE('',#8135,#7939,#9149,.T.);
#6546=EDGE_CURVE('',#8134,#7940,#9150,.T.);
#6547=EDGE_CURVE('',#8133,#7941,#9151,.T.);
#6548=EDGE_CURVE('',#8132,#7942,#9152,.T.);
#6549=EDGE_CURVE('',#8131,#7943,#9153,.T.);
#6550=EDGE_CURVE('',#8130,#7944,#9154,.T.);
#6551=EDGE_CURVE('',#8129,#7945,#9155,.T.);
#6552=EDGE_CURVE('',#8128,#7946,#9156,.T.);
#6553=EDGE_CURVE('',#8127,#7947,#9157,.T.);
#6554=EDGE_CURVE('',#8126,#7948,#9158,.T.);
#6555=EDGE_CURVE('',#8125,#7949,#9159,.T.);
#6556=EDGE_CURVE('',#8124,#7950,#9160,.T.);
#6557=EDGE_CURVE('',#8123,#7951,#9161,.T.);
#6558=EDGE_CURVE('',#8122,#7952,#9162,.T.);
#6559=EDGE_CURVE('',#8121,#7953,#9163,.T.);
#6560=EDGE_CURVE('',#8120,#7954,#9164,.T.);
#6561=EDGE_CURVE('',#8119,#7955,#9165,.T.);
#6562=EDGE_CURVE('',#8118,#7956,#9166,.T.);
#6563=EDGE_CURVE('',#8117,#7957,#9167,.T.);
#6564=EDGE_CURVE('',#8116,#7958,#9168,.T.);
#6565=EDGE_CURVE('',#8115,#7959,#9169,.T.);
#6566=EDGE_CURVE('',#8114,#7960,#9170,.T.);
#6567=EDGE_CURVE('',#8113,#7961,#9171,.T.);
#6568=EDGE_CURVE('',#8112,#7962,#9172,.T.);
#6569=EDGE_CURVE('',#8111,#7963,#9173,.T.);
#6570=EDGE_CURVE('',#8110,#7964,#9174,.T.);
#6571=EDGE_CURVE('',#8109,#7965,#9175,.T.);
#6572=EDGE_CURVE('',#8108,#7966,#9176,.T.);
#6573=EDGE_CURVE('',#8107,#7967,#9177,.T.);
#6574=EDGE_CURVE('',#8106,#7968,#9178,.T.);
#6575=EDGE_CURVE('',#8105,#7969,#9179,.T.);
#6576=EDGE_CURVE('',#8104,#7970,#9180,.T.);
#6577=EDGE_CURVE('',#8103,#7971,#9181,.T.);
#6578=EDGE_CURVE('',#8102,#7972,#9182,.T.);
#6579=EDGE_CURVE('',#8101,#7973,#9183,.T.);
#6580=EDGE_CURVE('',#8100,#7974,#9184,.T.);
#6581=EDGE_CURVE('',#8099,#7975,#9185,.T.);
#6582=EDGE_CURVE('',#8098,#7976,#9186,.T.);
#6583=EDGE_CURVE('',#8097,#7977,#9187,.T.);
#6584=EDGE_CURVE('',#8096,#7978,#9188,.T.);
#6585=EDGE_CURVE('',#8095,#7979,#9189,.T.);
#6586=EDGE_CURVE('',#8094,#7980,#9190,.T.);
#6587=EDGE_CURVE('',#8093,#7981,#9191,.T.);
#6588=EDGE_CURVE('',#8092,#7982,#9192,.T.);
#6589=EDGE_CURVE('',#8091,#7983,#9193,.T.);
#6590=EDGE_CURVE('',#8090,#7984,#9194,.T.);
#6591=EDGE_CURVE('',#8089,#7985,#9195,.T.);
#6592=EDGE_CURVE('',#8088,#7986,#9196,.T.);
#6593=EDGE_CURVE('',#8087,#7987,#9197,.T.);
#6594=EDGE_CURVE('',#8086,#7988,#9198,.T.);
#6595=EDGE_CURVE('',#8085,#7989,#9199,.T.);
#6596=EDGE_CURVE('',#8084,#7990,#9200,.T.);
#6597=EDGE_CURVE('',#8083,#7991,#9201,.T.);
#6598=EDGE_CURVE('',#8082,#7992,#9202,.T.);
#6599=EDGE_CURVE('',#8081,#7993,#9203,.T.);
#6600=EDGE_CURVE('',#8080,#7994,#9204,.T.);
#6601=EDGE_CURVE('',#8079,#7995,#9205,.T.);
#6602=EDGE_CURVE('',#8078,#7996,#9206,.T.);
#6603=EDGE_CURVE('',#8077,#7997,#9207,.T.);
#6604=EDGE_CURVE('',#8076,#7998,#9208,.T.);
#6605=EDGE_CURVE('',#8075,#7999,#9209,.T.);
#6606=EDGE_CURVE('',#8074,#8000,#9210,.T.);
#6607=EDGE_CURVE('',#8073,#8001,#9211,.T.);
#6608=EDGE_CURVE('',#8072,#8002,#9212,.T.);
#6609=EDGE_CURVE('',#8071,#8003,#9213,.T.);
#6610=EDGE_CURVE('',#8070,#8004,#9214,.T.);
#6611=EDGE_CURVE('',#8069,#8005,#9215,.T.);
#6612=EDGE_CURVE('',#8068,#8006,#9216,.T.);
#6613=EDGE_CURVE('',#8067,#8007,#9217,.T.);
#6614=EDGE_CURVE('',#8066,#8008,#9218,.T.);
#6615=EDGE_CURVE('',#8065,#8009,#9219,.T.);
#6616=EDGE_CURVE('',#8064,#8010,#9220,.T.);
#6617=EDGE_CURVE('',#8063,#8011,#9221,.T.);
#6618=EDGE_CURVE('',#8062,#8012,#9222,.T.);
#6619=EDGE_CURVE('',#8061,#8013,#9223,.T.);
#6620=EDGE_CURVE('',#8060,#8014,#9224,.T.);
#6621=EDGE_CURVE('',#8059,#8015,#9225,.T.);
#6622=EDGE_CURVE('',#8058,#8016,#9226,.T.);
#6623=EDGE_CURVE('',#8057,#8017,#9227,.T.);
#6624=EDGE_CURVE('',#8056,#8018,#9228,.T.);
#6625=EDGE_CURVE('',#8055,#8019,#9229,.T.);
#6626=EDGE_CURVE('',#8054,#8020,#9230,.T.);
#6627=EDGE_CURVE('',#8053,#8021,#9231,.T.);
#6628=EDGE_CURVE('',#8052,#8022,#9232,.T.);
#6629=EDGE_CURVE('',#8051,#8023,#9233,.T.);
#6630=EDGE_CURVE('',#8050,#8024,#9234,.T.);
#6631=EDGE_CURVE('',#8049,#8025,#9235,.T.);
#6632=EDGE_CURVE('',#8048,#8026,#9236,.T.);
#6633=EDGE_CURVE('',#8047,#8027,#9237,.T.);
#6634=EDGE_CURVE('',#8046,#8028,#9238,.T.);
#6635=EDGE_CURVE('',#8045,#8029,#9239,.T.);
#6636=EDGE_CURVE('',#8044,#8030,#9240,.T.);
#6637=EDGE_CURVE('',#8043,#8031,#9241,.T.);
#6638=EDGE_CURVE('',#8042,#8032,#9242,.T.);
#6639=EDGE_CURVE('',#8041,#8033,#9243,.T.);
#6640=EDGE_CURVE('',#8040,#8034,#9244,.T.);
#6641=EDGE_CURVE('',#8039,#8035,#9245,.T.);
#6642=EDGE_CURVE('',#8038,#7894,#9246,.T.);
#6643=EDGE_CURVE('',#7869,#7891,#743,.T.);
#6644=EDGE_CURVE('',#8181,#8181,#744,.T.);
#6645=EDGE_CURVE('',#8182,#8182,#745,.T.);
#6646=EDGE_CURVE('',#8183,#8183,#746,.T.);
#7867=VERTEX_POINT('',#33565);
#7868=VERTEX_POINT('',#33567);
#7869=VERTEX_POINT('',#33687);
#7870=VERTEX_POINT('',#33688);
#7871=VERTEX_POINT('',#33698);
#7872=VERTEX_POINT('',#33708);
#7873=VERTEX_POINT('',#33718);
#7874=VERTEX_POINT('',#33728);
#7875=VERTEX_POINT('',#33738);
#7876=VERTEX_POINT('',#33748);
#7877=VERTEX_POINT('',#33754);
#7878=VERTEX_POINT('',#33756);
#7879=VERTEX_POINT('',#33814);
#7880=VERTEX_POINT('',#33931);
#7881=VERTEX_POINT('',#33932);
#7882=VERTEX_POINT('',#33938);
#7883=VERTEX_POINT('',#33948);
#7884=VERTEX_POINT('',#33958);
#7885=VERTEX_POINT('',#33968);
#7886=VERTEX_POINT('',#33978);
#7887=VERTEX_POINT('',#33988);
#7888=VERTEX_POINT('',#33998);
#7889=VERTEX_POINT('',#34004);
#7890=VERTEX_POINT('',#34006);
#7891=VERTEX_POINT('',#34069);
#7892=VERTEX_POINT('',#34076);
#7893=VERTEX_POINT('',#34079);
#7894=VERTEX_POINT('',#34080);
#7895=VERTEX_POINT('',#34082);
#7896=VERTEX_POINT('',#34084);
#7897=VERTEX_POINT('',#34086);
#7898=VERTEX_POINT('',#34088);
#7899=VERTEX_POINT('',#34090);
#7900=VERTEX_POINT('',#34092);
#7901=VERTEX_POINT('',#34094);
#7902=VERTEX_POINT('',#34096);
#7903=VERTEX_POINT('',#34098);
#7904=VERTEX_POINT('',#34100);
#7905=VERTEX_POINT('',#34102);
#7906=VERTEX_POINT('',#34104);
#7907=VERTEX_POINT('',#34106);
#7908=VERTEX_POINT('',#34108);
#7909=VERTEX_POINT('',#34110);
#7910=VERTEX_POINT('',#34112);
#7911=VERTEX_POINT('',#34114);
#7912=VERTEX_POINT('',#34116);
#7913=VERTEX_POINT('',#34118);
#7914=VERTEX_POINT('',#34120);
#7915=VERTEX_POINT('',#34122);
#7916=VERTEX_POINT('',#34124);
#7917=VERTEX_POINT('',#34126);
#7918=VERTEX_POINT('',#34128);
#7919=VERTEX_POINT('',#34130);
#7920=VERTEX_POINT('',#34132);
#7921=VERTEX_POINT('',#34134);
#7922=VERTEX_POINT('',#34136);
#7923=VERTEX_POINT('',#34138);
#7924=VERTEX_POINT('',#34140);
#7925=VERTEX_POINT('',#34142);
#7926=VERTEX_POINT('',#34144);
#7927=VERTEX_POINT('',#34146);
#7928=VERTEX_POINT('',#34148);
#7929=VERTEX_POINT('',#34150);
#7930=VERTEX_POINT('',#34152);
#7931=VERTEX_POINT('',#34154);
#7932=VERTEX_POINT('',#34156);
#7933=VERTEX_POINT('',#34158);
#7934=VERTEX_POINT('',#34160);
#7935=VERTEX_POINT('',#34162);
#7936=VERTEX_POINT('',#34164);
#7937=VERTEX_POINT('',#34166);
#7938=VERTEX_POINT('',#34168);
#7939=VERTEX_POINT('',#34170);
#7940=VERTEX_POINT('',#34172);
#7941=VERTEX_POINT('',#34174);
#7942=VERTEX_POINT('',#34176);
#7943=VERTEX_POINT('',#34178);
#7944=VERTEX_POINT('',#34180);
#7945=VERTEX_POINT('',#34182);
#7946=VERTEX_POINT('',#34184);
#7947=VERTEX_POINT('',#34186);
#7948=VERTEX_POINT('',#34188);
#7949=VERTEX_POINT('',#34190);
#7950=VERTEX_POINT('',#34192);
#7951=VERTEX_POINT('',#34194);
#7952=VERTEX_POINT('',#34196);
#7953=VERTEX_POINT('',#34198);
#7954=VERTEX_POINT('',#34200);
#7955=VERTEX_POINT('',#34202);
#7956=VERTEX_POINT('',#34204);
#7957=VERTEX_POINT('',#34206);
#7958=VERTEX_POINT('',#34208);
#7959=VERTEX_POINT('',#34210);
#7960=VERTEX_POINT('',#34212);
#7961=VERTEX_POINT('',#34214);
#7962=VERTEX_POINT('',#34216);
#7963=VERTEX_POINT('',#34218);
#7964=VERTEX_POINT('',#34220);
#7965=VERTEX_POINT('',#34222);
#7966=VERTEX_POINT('',#34224);
#7967=VERTEX_POINT('',#34226);
#7968=VERTEX_POINT('',#34228);
#7969=VERTEX_POINT('',#34230);
#7970=VERTEX_POINT('',#34232);
#7971=VERTEX_POINT('',#34234);
#7972=VERTEX_POINT('',#34236);
#7973=VERTEX_POINT('',#34238);
#7974=VERTEX_POINT('',#34240);
#7975=VERTEX_POINT('',#34242);
#7976=VERTEX_POINT('',#34244);
#7977=VERTEX_POINT('',#34246);
#7978=VERTEX_POINT('',#34248);
#7979=VERTEX_POINT('',#34250);
#7980=VERTEX_POINT('',#34252);
#7981=VERTEX_POINT('',#34254);
#7982=VERTEX_POINT('',#34256);
#7983=VERTEX_POINT('',#34258);
#7984=VERTEX_POINT('',#34260);
#7985=VERTEX_POINT('',#34262);
#7986=VERTEX_POINT('',#34264);
#7987=VERTEX_POINT('',#34266);
#7988=VERTEX_POINT('',#34268);
#7989=VERTEX_POINT('',#34270);
#7990=VERTEX_POINT('',#34272);
#7991=VERTEX_POINT('',#34274);
#7992=VERTEX_POINT('',#34276);
#7993=VERTEX_POINT('',#34278);
#7994=VERTEX_POINT('',#34280);
#7995=VERTEX_POINT('',#34282);
#7996=VERTEX_POINT('',#34284);
#7997=VERTEX_POINT('',#34286);
#7998=VERTEX_POINT('',#34288);
#7999=VERTEX_POINT('',#34290);
#8000=VERTEX_POINT('',#34292);
#8001=VERTEX_POINT('',#34294);
#8002=VERTEX_POINT('',#34296);
#8003=VERTEX_POINT('',#34298);
#8004=VERTEX_POINT('',#34300);
#8005=VERTEX_POINT('',#34302);
#8006=VERTEX_POINT('',#34304);
#8007=VERTEX_POINT('',#34306);
#8008=VERTEX_POINT('',#34308);
#8009=VERTEX_POINT('',#34310);
#8010=VERTEX_POINT('',#34312);
#8011=VERTEX_POINT('',#34314);
#8012=VERTEX_POINT('',#34316);
#8013=VERTEX_POINT('',#34318);
#8014=VERTEX_POINT('',#34320);
#8015=VERTEX_POINT('',#34322);
#8016=VERTEX_POINT('',#34324);
#8017=VERTEX_POINT('',#34326);
#8018=VERTEX_POINT('',#34328);
#8019=VERTEX_POINT('',#34330);
#8020=VERTEX_POINT('',#34332);
#8021=VERTEX_POINT('',#34334);
#8022=VERTEX_POINT('',#34336);
#8023=VERTEX_POINT('',#34338);
#8024=VERTEX_POINT('',#34340);
#8025=VERTEX_POINT('',#34342);
#8026=VERTEX_POINT('',#34344);
#8027=VERTEX_POINT('',#34346);
#8028=VERTEX_POINT('',#34348);
#8029=VERTEX_POINT('',#34350);
#8030=VERTEX_POINT('',#34352);
#8031=VERTEX_POINT('',#34354);
#8032=VERTEX_POINT('',#34356);
#8033=VERTEX_POINT('',#34358);
#8034=VERTEX_POINT('',#34360);
#8035=VERTEX_POINT('',#34362);
#8036=VERTEX_POINT('',#34365);
#8037=VERTEX_POINT('',#34368);
#8038=VERTEX_POINT('',#34369);
#8039=VERTEX_POINT('',#34371);
#8040=VERTEX_POINT('',#34373);
#8041=VERTEX_POINT('',#34375);
#8042=VERTEX_POINT('',#34377);
#8043=VERTEX_POINT('',#34379);
#8044=VERTEX_POINT('',#34381);
#8045=VERTEX_POINT('',#34383);
#8046=VERTEX_POINT('',#34385);
#8047=VERTEX_POINT('',#34387);
#8048=VERTEX_POINT('',#34389);
#8049=VERTEX_POINT('',#34391);
#8050=VERTEX_POINT('',#34393);
#8051=VERTEX_POINT('',#34395);
#8052=VERTEX_POINT('',#34397);
#8053=VERTEX_POINT('',#34399);
#8054=VERTEX_POINT('',#34401);
#8055=VERTEX_POINT('',#34403);
#8056=VERTEX_POINT('',#34405);
#8057=VERTEX_POINT('',#34407);
#8058=VERTEX_POINT('',#34409);
#8059=VERTEX_POINT('',#34411);
#8060=VERTEX_POINT('',#34413);
#8061=VERTEX_POINT('',#34415);
#8062=VERTEX_POINT('',#34417);
#8063=VERTEX_POINT('',#34419);
#8064=VERTEX_POINT('',#34421);
#8065=VERTEX_POINT('',#34423);
#8066=VERTEX_POINT('',#34425);
#8067=VERTEX_POINT('',#34427);
#8068=VERTEX_POINT('',#34429);
#8069=VERTEX_POINT('',#34431);
#8070=VERTEX_POINT('',#34433);
#8071=VERTEX_POINT('',#34435);
#8072=VERTEX_POINT('',#34437);
#8073=VERTEX_POINT('',#34439);
#8074=VERTEX_POINT('',#34441);
#8075=VERTEX_POINT('',#34443);
#8076=VERTEX_POINT('',#34445);
#8077=VERTEX_POINT('',#34447);
#8078=VERTEX_POINT('',#34449);
#8079=VERTEX_POINT('',#34451);
#8080=VERTEX_POINT('',#34453);
#8081=VERTEX_POINT('',#34455);
#8082=VERTEX_POINT('',#34457);
#8083=VERTEX_POINT('',#34459);
#8084=VERTEX_POINT('',#34461);
#8085=VERTEX_POINT('',#34463);
#8086=VERTEX_POINT('',#34465);
#8087=VERTEX_POINT('',#34467);
#8088=VERTEX_POINT('',#34469);
#8089=VERTEX_POINT('',#34471);
#8090=VERTEX_POINT('',#34473);
#8091=VERTEX_POINT('',#34475);
#8092=VERTEX_POINT('',#34477);
#8093=VERTEX_POINT('',#34479);
#8094=VERTEX_POINT('',#34481);
#8095=VERTEX_POINT('',#34483);
#8096=VERTEX_POINT('',#34485);
#8097=VERTEX_POINT('',#34487);
#8098=VERTEX_POINT('',#34489);
#8099=VERTEX_POINT('',#34491);
#8100=VERTEX_POINT('',#34493);
#8101=VERTEX_POINT('',#34495);
#8102=VERTEX_POINT('',#34497);
#8103=VERTEX_POINT('',#34499);
#8104=VERTEX_POINT('',#34501);
#8105=VERTEX_POINT('',#34503);
#8106=VERTEX_POINT('',#34505);
#8107=VERTEX_POINT('',#34507);
#8108=VERTEX_POINT('',#34509);
#8109=VERTEX_POINT('',#34511);
#8110=VERTEX_POINT('',#34513);
#8111=VERTEX_POINT('',#34515);
#8112=VERTEX_POINT('',#34517);
#8113=VERTEX_POINT('',#34519);
#8114=VERTEX_POINT('',#34521);
#8115=VERTEX_POINT('',#34523);
#8116=VERTEX_POINT('',#34525);
#8117=VERTEX_POINT('',#34527);
#8118=VERTEX_POINT('',#34529);
#8119=VERTEX_POINT('',#34531);
#8120=VERTEX_POINT('',#34533);
#8121=VERTEX_POINT('',#34535);
#8122=VERTEX_POINT('',#34537);
#8123=VERTEX_POINT('',#34539);
#8124=VERTEX_POINT('',#34541);
#8125=VERTEX_POINT('',#34543);
#8126=VERTEX_POINT('',#34545);
#8127=VERTEX_POINT('',#34547);
#8128=VERTEX_POINT('',#34549);
#8129=VERTEX_POINT('',#34551);
#8130=VERTEX_POINT('',#34553);
#8131=VERTEX_POINT('',#34555);
#8132=VERTEX_POINT('',#34557);
#8133=VERTEX_POINT('',#34559);
#8134=VERTEX_POINT('',#34561);
#8135=VERTEX_POINT('',#34563);
#8136=VERTEX_POINT('',#34565);
#8137=VERTEX_POINT('',#34567);
#8138=VERTEX_POINT('',#34569);
#8139=VERTEX_POINT('',#34571);
#8140=VERTEX_POINT('',#34573);
#8141=VERTEX_POINT('',#34575);
#8142=VERTEX_POINT('',#34577);
#8143=VERTEX_POINT('',#34579);
#8144=VERTEX_POINT('',#34581);
#8145=VERTEX_POINT('',#34583);
#8146=VERTEX_POINT('',#34585);
#8147=VERTEX_POINT('',#34587);
#8148=VERTEX_POINT('',#34589);
#8149=VERTEX_POINT('',#34591);
#8150=VERTEX_POINT('',#34593);
#8151=VERTEX_POINT('',#34595);
#8152=VERTEX_POINT('',#34597);
#8153=VERTEX_POINT('',#34599);
#8154=VERTEX_POINT('',#34601);
#8155=VERTEX_POINT('',#34603);
#8156=VERTEX_POINT('',#34605);
#8157=VERTEX_POINT('',#34607);
#8158=VERTEX_POINT('',#34609);
#8159=VERTEX_POINT('',#34611);
#8160=VERTEX_POINT('',#34613);
#8161=VERTEX_POINT('',#34615);
#8162=VERTEX_POINT('',#34617);
#8163=VERTEX_POINT('',#34619);
#8164=VERTEX_POINT('',#34621);
#8165=VERTEX_POINT('',#34623);
#8166=VERTEX_POINT('',#34625);
#8167=VERTEX_POINT('',#34627);
#8168=VERTEX_POINT('',#34629);
#8169=VERTEX_POINT('',#34631);
#8170=VERTEX_POINT('',#34633);
#8171=VERTEX_POINT('',#34635);
#8172=VERTEX_POINT('',#34637);
#8173=VERTEX_POINT('',#34639);
#8174=VERTEX_POINT('',#34641);
#8175=VERTEX_POINT('',#34643);
#8176=VERTEX_POINT('',#34645);
#8177=VERTEX_POINT('',#34647);
#8178=VERTEX_POINT('',#34649);
#8179=VERTEX_POINT('',#34651);
#8180=VERTEX_POINT('',#34654);
#8181=VERTEX_POINT('',#34944);
#8182=VERTEX_POINT('',#34949);
#8183=VERTEX_POINT('',#34952);
#8903=LINE('',#33755,#9731);
#8904=LINE('',#33815,#9732);
#8905=LINE('',#33930,#9733);
#8906=LINE('',#34005,#9734);
#8907=LINE('',#34065,#9735);
#8908=LINE('',#34066,#9736);
#8909=LINE('',#34068,#9737);
#8910=LINE('',#34070,#9738);
#8911=LINE('',#34072,#9739);
#8912=LINE('',#34078,#9740);
#8913=LINE('',#34083,#9741);
#8914=LINE('',#34085,#9742);
#8915=LINE('',#34089,#9743);
#8916=LINE('',#34091,#9744);
#8917=LINE('',#34095,#9745);
#8918=LINE('',#34097,#9746);
#8919=LINE('',#34101,#9747);
#8920=LINE('',#34103,#9748);
#8921=LINE('',#34107,#9749);
#8922=LINE('',#34109,#9750);
#8923=LINE('',#34113,#9751);
#8924=LINE('',#34115,#9752);
#8925=LINE('',#34119,#9753);
#8926=LINE('',#34121,#9754);
#8927=LINE('',#34125,#9755);
#8928=LINE('',#34127,#9756);
#8929=LINE('',#34131,#9757);
#8930=LINE('',#34133,#9758);
#8931=LINE('',#34137,#9759);
#8932=LINE('',#34139,#9760);
#8933=LINE('',#34143,#9761);
#8934=LINE('',#34145,#9762);
#8935=LINE('',#34149,#9763);
#8936=LINE('',#34151,#9764);
#8937=LINE('',#34155,#9765);
#8938=LINE('',#34157,#9766);
#8939=LINE('',#34161,#9767);
#8940=LINE('',#34163,#9768);
#8941=LINE('',#34167,#9769);
#8942=LINE('',#34169,#9770);
#8943=LINE('',#34173,#9771);
#8944=LINE('',#34175,#9772);
#8945=LINE('',#34179,#9773);
#8946=LINE('',#34181,#9774);
#8947=LINE('',#34185,#9775);
#8948=LINE('',#34187,#9776);
#8949=LINE('',#34191,#9777);
#8950=LINE('',#34193,#9778);
#8951=LINE('',#34197,#9779);
#8952=LINE('',#34199,#9780);
#8953=LINE('',#34203,#9781);
#8954=LINE('',#34205,#9782);
#8955=LINE('',#34209,#9783);
#8956=LINE('',#34211,#9784);
#8957=LINE('',#34215,#9785);
#8958=LINE('',#34217,#9786);
#8959=LINE('',#34221,#9787);
#8960=LINE('',#34223,#9788);
#8961=LINE('',#34227,#9789);
#8962=LINE('',#34229,#9790);
#8963=LINE('',#34233,#9791);
#8964=LINE('',#34235,#9792);
#8965=LINE('',#34239,#9793);
#8966=LINE('',#34241,#9794);
#8967=LINE('',#34245,#9795);
#8968=LINE('',#34247,#9796);
#8969=LINE('',#34251,#9797);
#8970=LINE('',#34253,#9798);
#8971=LINE('',#34257,#9799);
#8972=LINE('',#34259,#9800);
#8973=LINE('',#34263,#9801);
#8974=LINE('',#34265,#9802);
#8975=LINE('',#34269,#9803);
#8976=LINE('',#34271,#9804);
#8977=LINE('',#34275,#9805);
#8978=LINE('',#34277,#9806);
#8979=LINE('',#34281,#9807);
#8980=LINE('',#34283,#9808);
#8981=LINE('',#34287,#9809);
#8982=LINE('',#34289,#9810);
#8983=LINE('',#34293,#9811);
#8984=LINE('',#34295,#9812);
#8985=LINE('',#34299,#9813);
#8986=LINE('',#34301,#9814);
#8987=LINE('',#34305,#9815);
#8988=LINE('',#34307,#9816);
#8989=LINE('',#34311,#9817);
#8990=LINE('',#34313,#9818);
#8991=LINE('',#34317,#9819);
#8992=LINE('',#34319,#9820);
#8993=LINE('',#34323,#9821);
#8994=LINE('',#34325,#9822);
#8995=LINE('',#34329,#9823);
#8996=LINE('',#34331,#9824);
#8997=LINE('',#34335,#9825);
#8998=LINE('',#34337,#9826);
#8999=LINE('',#34339,#9827);
#9000=LINE('',#34341,#9828);
#9001=LINE('',#34345,#9829);
#9002=LINE('',#34347,#9830);
#9003=LINE('',#34351,#9831);
#9004=LINE('',#34353,#9832);
#9005=LINE('',#34357,#9833);
#9006=LINE('',#34359,#9834);
#9007=LINE('',#34363,#9835);
#9008=LINE('',#34367,#9836);
#9009=LINE('',#34370,#9837);
#9010=LINE('',#34374,#9838);
#9011=LINE('',#34376,#9839);
#9012=LINE('',#34380,#9840);
#9013=LINE('',#34382,#9841);
#9014=LINE('',#34386,#9842);
#9015=LINE('',#34388,#9843);
#9016=LINE('',#34392,#9844);
#9017=LINE('',#34394,#9845);
#9018=LINE('',#34396,#9846);
#9019=LINE('',#34398,#9847);
#9020=LINE('',#34402,#9848);
#9021=LINE('',#34404,#9849);
#9022=LINE('',#34408,#9850);
#9023=LINE('',#34410,#9851);
#9024=LINE('',#34414,#9852);
#9025=LINE('',#34416,#9853);
#9026=LINE('',#34420,#9854);
#9027=LINE('',#34422,#9855);
#9028=LINE('',#34426,#9856);
#9029=LINE('',#34428,#9857);
#9030=LINE('',#34432,#9858);
#9031=LINE('',#34434,#9859);
#9032=LINE('',#34438,#9860);
#9033=LINE('',#34440,#9861);
#9034=LINE('',#34444,#9862);
#9035=LINE('',#34446,#9863);
#9036=LINE('',#34450,#9864);
#9037=LINE('',#34452,#9865);
#9038=LINE('',#34456,#9866);
#9039=LINE('',#34458,#9867);
#9040=LINE('',#34462,#9868);
#9041=LINE('',#34464,#9869);
#9042=LINE('',#34468,#9870);
#9043=LINE('',#34470,#9871);
#9044=LINE('',#34474,#9872);
#9045=LINE('',#34476,#9873);
#9046=LINE('',#34480,#9874);
#9047=LINE('',#34482,#9875);
#9048=LINE('',#34486,#9876);
#9049=LINE('',#34488,#9877);
#9050=LINE('',#34492,#9878);
#9051=LINE('',#34494,#9879);
#9052=LINE('',#34498,#9880);
#9053=LINE('',#34500,#9881);
#9054=LINE('',#34504,#9882);
#9055=LINE('',#34506,#9883);
#9056=LINE('',#34510,#9884);
#9057=LINE('',#34512,#9885);
#9058=LINE('',#34516,#9886);
#9059=LINE('',#34518,#9887);
#9060=LINE('',#34522,#9888);
#9061=LINE('',#34524,#9889);
#9062=LINE('',#34528,#9890);
#9063=LINE('',#34530,#9891);
#9064=LINE('',#34534,#9892);
#9065=LINE('',#34536,#9893);
#9066=LINE('',#34540,#9894);
#9067=LINE('',#34542,#9895);
#9068=LINE('',#34546,#9896);
#9069=LINE('',#34548,#9897);
#9070=LINE('',#34552,#9898);
#9071=LINE('',#34554,#9899);
#9072=LINE('',#34558,#9900);
#9073=LINE('',#34560,#9901);
#9074=LINE('',#34564,#9902);
#9075=LINE('',#34566,#9903);
#9076=LINE('',#34570,#9904);
#9077=LINE('',#34572,#9905);
#9078=LINE('',#34576,#9906);
#9079=LINE('',#34578,#9907);
#9080=LINE('',#34582,#9908);
#9081=LINE('',#34584,#9909);
#9082=LINE('',#34588,#9910);
#9083=LINE('',#34590,#9911);
#9084=LINE('',#34594,#9912);
#9085=LINE('',#34596,#9913);
#9086=LINE('',#34600,#9914);
#9087=LINE('',#34602,#9915);
#9088=LINE('',#34606,#9916);
#9089=LINE('',#34608,#9917);
#9090=LINE('',#34612,#9918);
#9091=LINE('',#34614,#9919);
#9092=LINE('',#34618,#9920);
#9093=LINE('',#34620,#9921);
#9094=LINE('',#34624,#9922);
#9095=LINE('',#34626,#9923);
#9096=LINE('',#34630,#9924);
#9097=LINE('',#34632,#9925);
#9098=LINE('',#34636,#9926);
#9099=LINE('',#34638,#9927);
#9100=LINE('',#34642,#9928);
#9101=LINE('',#34644,#9929);
#9102=LINE('',#34648,#9930);
#9103=LINE('',#34650,#9931);
#9104=LINE('',#34656,#9932);
#9105=LINE('',#34657,#9933);
#9106=LINE('',#34659,#9934);
#9107=LINE('',#34661,#9935);
#9108=LINE('',#34663,#9936);
#9109=LINE('',#34665,#9937);
#9110=LINE('',#34667,#9938);
#9111=LINE('',#34669,#9939);
#9112=LINE('',#34671,#9940);
#9113=LINE('',#34673,#9941);
#9114=LINE('',#34675,#9942);
#9115=LINE('',#34677,#9943);
#9116=LINE('',#34679,#9944);
#9117=LINE('',#34681,#9945);
#9118=LINE('',#34683,#9946);
#9119=LINE('',#34685,#9947);
#9120=LINE('',#34687,#9948);
#9121=LINE('',#34689,#9949);
#9122=LINE('',#34691,#9950);
#9123=LINE('',#34693,#9951);
#9124=LINE('',#34695,#9952);
#9125=LINE('',#34697,#9953);
#9126=LINE('',#34699,#9954);
#9127=LINE('',#34701,#9955);
#9128=LINE('',#34703,#9956);
#9129=LINE('',#34705,#9957);
#9130=LINE('',#34707,#9958);
#9131=LINE('',#34709,#9959);
#9132=LINE('',#34711,#9960);
#9133=LINE('',#34713,#9961);
#9134=LINE('',#34715,#9962);
#9135=LINE('',#34717,#9963);
#9136=LINE('',#34719,#9964);
#9137=LINE('',#34721,#9965);
#9138=LINE('',#34723,#9966);
#9139=LINE('',#34725,#9967);
#9140=LINE('',#34727,#9968);
#9141=LINE('',#34729,#9969);
#9142=LINE('',#34731,#9970);
#9143=LINE('',#34733,#9971);
#9144=LINE('',#34735,#9972);
#9145=LINE('',#34737,#9973);
#9146=LINE('',#34739,#9974);
#9147=LINE('',#34741,#9975);
#9148=LINE('',#34743,#9976);
#9149=LINE('',#34745,#9977);
#9150=LINE('',#34747,#9978);
#9151=LINE('',#34749,#9979);
#9152=LINE('',#34751,#9980);
#9153=LINE('',#34753,#9981);
#9154=LINE('',#34755,#9982);
#9155=LINE('',#34757,#9983);
#9156=LINE('',#34759,#9984);
#9157=LINE('',#34761,#9985);
#9158=LINE('',#34763,#9986);
#9159=LINE('',#34765,#9987);
#9160=LINE('',#34767,#9988);
#9161=LINE('',#34769,#9989);
#9162=LINE('',#34771,#9990);
#9163=LINE('',#34773,#9991);
#9164=LINE('',#34775,#9992);
#9165=LINE('',#34777,#9993);
#9166=LINE('',#34779,#9994);
#9167=LINE('',#34781,#9995);
#9168=LINE('',#34783,#9996);
#9169=LINE('',#34785,#9997);
#9170=LINE('',#34787,#9998);
#9171=LINE('',#34789,#9999);
#9172=LINE('',#34791,#10000);
#9173=LINE('',#34793,#10001);
#9174=LINE('',#34795,#10002);
#9175=LINE('',#34797,#10003);
#9176=LINE('',#34799,#10004);
#9177=LINE('',#34801,#10005);
#9178=LINE('',#34803,#10006);
#9179=LINE('',#34805,#10007);
#9180=LINE('',#34807,#10008);
#9181=LINE('',#34809,#10009);
#9182=LINE('',#34811,#10010);
#9183=LINE('',#34813,#10011);
#9184=LINE('',#34815,#10012);
#9185=LINE('',#34817,#10013);
#9186=LINE('',#34819,#10014);
#9187=LINE('',#34821,#10015);
#9188=LINE('',#34823,#10016);
#9189=LINE('',#34825,#10017);
#9190=LINE('',#34827,#10018);
#9191=LINE('',#34829,#10019);
#9192=LINE('',#34831,#10020);
#9193=LINE('',#34833,#10021);
#9194=LINE('',#34835,#10022);
#9195=LINE('',#34837,#10023);
#9196=LINE('',#34839,#10024);
#9197=LINE('',#34841,#10025);
#9198=LINE('',#34843,#10026);
#9199=LINE('',#34845,#10027);
#9200=LINE('',#34847,#10028);
#9201=LINE('',#34849,#10029);
#9202=LINE('',#34851,#10030);
#9203=LINE('',#34853,#10031);
#9204=LINE('',#34855,#10032);
#9205=LINE('',#34857,#10033);
#9206=LINE('',#34859,#10034);
#9207=LINE('',#34861,#10035);
#9208=LINE('',#34863,#10036);
#9209=LINE('',#34865,#10037);
#9210=LINE('',#34867,#10038);
#9211=LINE('',#34869,#10039);
#9212=LINE('',#34871,#10040);
#9213=LINE('',#34873,#10041);
#9214=LINE('',#34875,#10042);
#9215=LINE('',#34877,#10043);
#9216=LINE('',#34879,#10044);
#9217=LINE('',#34881,#10045);
#9218=LINE('',#34883,#10046);
#9219=LINE('',#34885,#10047);
#9220=LINE('',#34887,#10048);
#9221=LINE('',#34889,#10049);
#9222=LINE('',#34891,#10050);
#9223=LINE('',#34893,#10051);
#9224=LINE('',#34895,#10052);
#9225=LINE('',#34897,#10053);
#9226=LINE('',#34899,#10054);
#9227=LINE('',#34901,#10055);
#9228=LINE('',#34903,#10056);
#9229=LINE('',#34905,#10057);
#9230=LINE('',#34907,#10058);
#9231=LINE('',#34909,#10059);
#9232=LINE('',#34911,#10060);
#9233=LINE('',#34913,#10061);
#9234=LINE('',#34915,#10062);
#9235=LINE('',#34917,#10063);
#9236=LINE('',#34919,#10064);
#9237=LINE('',#34921,#10065);
#9238=LINE('',#34923,#10066);
#9239=LINE('',#34925,#10067);
#9240=LINE('',#34927,#10068);
#9241=LINE('',#34929,#10069);
#9242=LINE('',#34931,#10070);
#9243=LINE('',#34933,#10071);
#9244=LINE('',#34935,#10072);
#9245=LINE('',#34937,#10073);
#9246=LINE('',#34939,#10074);
#9731=VECTOR('',#16587,1.);
#9732=VECTOR('',#16588,1.);
#9733=VECTOR('',#16589,1.);
#9734=VECTOR('',#16590,1.);
#9735=VECTOR('',#16593,1.);
#9736=VECTOR('',#16594,1.);
#9737=VECTOR('',#16597,1.);
#9738=VECTOR('',#16598,1.);
#9739=VECTOR('',#16601,1.);
#9740=VECTOR('',#16610,1.);
#9741=VECTOR('',#16613,1.);
#9742=VECTOR('',#16614,1.);
#9743=VECTOR('',#16617,1.);
#9744=VECTOR('',#16618,1.);
#9745=VECTOR('',#16621,1.);
#9746=VECTOR('',#16622,1.);
#9747=VECTOR('',#16625,1.);
#9748=VECTOR('',#16626,1.);
#9749=VECTOR('',#16629,1.);
#9750=VECTOR('',#16630,1.);
#9751=VECTOR('',#16633,1.);
#9752=VECTOR('',#16634,1.);
#9753=VECTOR('',#16637,1.);
#9754=VECTOR('',#16638,1.);
#9755=VECTOR('',#16641,1.);
#9756=VECTOR('',#16642,1.);
#9757=VECTOR('',#16645,1.);
#9758=VECTOR('',#16646,1.);
#9759=VECTOR('',#16649,1.);
#9760=VECTOR('',#16650,1.);
#9761=VECTOR('',#16653,1.);
#9762=VECTOR('',#16654,1.);
#9763=VECTOR('',#16657,1.);
#9764=VECTOR('',#16658,1.);
#9765=VECTOR('',#16661,1.);
#9766=VECTOR('',#16662,1.);
#9767=VECTOR('',#16665,1.);
#9768=VECTOR('',#16666,1.);
#9769=VECTOR('',#16669,1.);
#9770=VECTOR('',#16670,1.);
#9771=VECTOR('',#16673,1.);
#9772=VECTOR('',#16674,1.);
#9773=VECTOR('',#16677,1.);
#9774=VECTOR('',#16678,1.);
#9775=VECTOR('',#16681,1.);
#9776=VECTOR('',#16682,1.);
#9777=VECTOR('',#16685,1.);
#9778=VECTOR('',#16686,1.);
#9779=VECTOR('',#16689,1.);
#9780=VECTOR('',#16690,1.);
#9781=VECTOR('',#16693,1.);
#9782=VECTOR('',#16694,1.);
#9783=VECTOR('',#16697,1.);
#9784=VECTOR('',#16698,1.);
#9785=VECTOR('',#16701,1.);
#9786=VECTOR('',#16702,1.);
#9787=VECTOR('',#16705,1.);
#9788=VECTOR('',#16706,1.);
#9789=VECTOR('',#16709,1.);
#9790=VECTOR('',#16710,1.);
#9791=VECTOR('',#16713,1.);
#9792=VECTOR('',#16714,1.);
#9793=VECTOR('',#16717,1.);
#9794=VECTOR('',#16718,1.);
#9795=VECTOR('',#16721,1.);
#9796=VECTOR('',#16722,1.);
#9797=VECTOR('',#16725,1.);
#9798=VECTOR('',#16726,1.);
#9799=VECTOR('',#16729,1.);
#9800=VECTOR('',#16730,1.);
#9801=VECTOR('',#16733,1.);
#9802=VECTOR('',#16734,1.);
#9803=VECTOR('',#16737,1.);
#9804=VECTOR('',#16738,1.);
#9805=VECTOR('',#16741,1.);
#9806=VECTOR('',#16742,1.);
#9807=VECTOR('',#16745,1.);
#9808=VECTOR('',#16746,1.);
#9809=VECTOR('',#16749,1.);
#9810=VECTOR('',#16750,1.);
#9811=VECTOR('',#16753,1.);
#9812=VECTOR('',#16754,1.);
#9813=VECTOR('',#16757,1.);
#9814=VECTOR('',#16758,1.);
#9815=VECTOR('',#16761,1.);
#9816=VECTOR('',#16762,1.);
#9817=VECTOR('',#16765,1.);
#9818=VECTOR('',#16766,1.);
#9819=VECTOR('',#16769,1.);
#9820=VECTOR('',#16770,1.);
#9821=VECTOR('',#16773,1.);
#9822=VECTOR('',#16774,1.);
#9823=VECTOR('',#16777,1.);
#9824=VECTOR('',#16778,1.);
#9825=VECTOR('',#16781,1.);
#9826=VECTOR('',#16782,1.);
#9827=VECTOR('',#16783,1.);
#9828=VECTOR('',#16784,1.);
#9829=VECTOR('',#16787,1.);
#9830=VECTOR('',#16788,1.);
#9831=VECTOR('',#16791,1.);
#9832=VECTOR('',#16792,1.);
#9833=VECTOR('',#16795,1.);
#9834=VECTOR('',#16796,1.);
#9835=VECTOR('',#16799,1.);
#9836=VECTOR('',#16804,1.);
#9837=VECTOR('',#16805,1.);
#9838=VECTOR('',#16808,1.);
#9839=VECTOR('',#16809,1.);
#9840=VECTOR('',#16812,1.);
#9841=VECTOR('',#16813,1.);
#9842=VECTOR('',#16816,1.);
#9843=VECTOR('',#16817,1.);
#9844=VECTOR('',#16820,1.);
#9845=VECTOR('',#16821,1.);
#9846=VECTOR('',#16822,1.);
#9847=VECTOR('',#16823,1.);
#9848=VECTOR('',#16826,1.);
#9849=VECTOR('',#16827,1.);
#9850=VECTOR('',#16830,1.);
#9851=VECTOR('',#16831,1.);
#9852=VECTOR('',#16834,1.);
#9853=VECTOR('',#16835,1.);
#9854=VECTOR('',#16838,1.);
#9855=VECTOR('',#16839,1.);
#9856=VECTOR('',#16842,1.);
#9857=VECTOR('',#16843,1.);
#9858=VECTOR('',#16846,1.);
#9859=VECTOR('',#16847,1.);
#9860=VECTOR('',#16850,1.);
#9861=VECTOR('',#16851,1.);
#9862=VECTOR('',#16854,1.);
#9863=VECTOR('',#16855,1.);
#9864=VECTOR('',#16858,1.);
#9865=VECTOR('',#16859,1.);
#9866=VECTOR('',#16862,1.);
#9867=VECTOR('',#16863,1.);
#9868=VECTOR('',#16866,1.);
#9869=VECTOR('',#16867,1.);
#9870=VECTOR('',#16870,1.);
#9871=VECTOR('',#16871,1.);
#9872=VECTOR('',#16874,1.);
#9873=VECTOR('',#16875,1.);
#9874=VECTOR('',#16878,1.);
#9875=VECTOR('',#16879,1.);
#9876=VECTOR('',#16882,1.);
#9877=VECTOR('',#16883,1.);
#9878=VECTOR('',#16886,1.);
#9879=VECTOR('',#16887,1.);
#9880=VECTOR('',#16890,1.);
#9881=VECTOR('',#16891,1.);
#9882=VECTOR('',#16894,1.);
#9883=VECTOR('',#16895,1.);
#9884=VECTOR('',#16898,1.);
#9885=VECTOR('',#16899,1.);
#9886=VECTOR('',#16902,1.);
#9887=VECTOR('',#16903,1.);
#9888=VECTOR('',#16906,1.);
#9889=VECTOR('',#16907,1.);
#9890=VECTOR('',#16910,1.);
#9891=VECTOR('',#16911,1.);
#9892=VECTOR('',#16914,1.);
#9893=VECTOR('',#16915,1.);
#9894=VECTOR('',#16918,1.);
#9895=VECTOR('',#16919,1.);
#9896=VECTOR('',#16922,1.);
#9897=VECTOR('',#16923,1.);
#9898=VECTOR('',#16926,1.);
#9899=VECTOR('',#16927,1.);
#9900=VECTOR('',#16930,1.);
#9901=VECTOR('',#16931,1.);
#9902=VECTOR('',#16934,1.);
#9903=VECTOR('',#16935,1.);
#9904=VECTOR('',#16938,1.);
#9905=VECTOR('',#16939,1.);
#9906=VECTOR('',#16942,1.);
#9907=VECTOR('',#16943,1.);
#9908=VECTOR('',#16946,1.);
#9909=VECTOR('',#16947,1.);
#9910=VECTOR('',#16950,1.);
#9911=VECTOR('',#16951,1.);
#9912=VECTOR('',#16954,1.);
#9913=VECTOR('',#16955,1.);
#9914=VECTOR('',#16958,1.);
#9915=VECTOR('',#16959,1.);
#9916=VECTOR('',#16962,1.);
#9917=VECTOR('',#16963,1.);
#9918=VECTOR('',#16966,1.);
#9919=VECTOR('',#16967,1.);
#9920=VECTOR('',#16970,1.);
#9921=VECTOR('',#16971,1.);
#9922=VECTOR('',#16974,1.);
#9923=VECTOR('',#16975,1.);
#9924=VECTOR('',#16978,1.);
#9925=VECTOR('',#16979,1.);
#9926=VECTOR('',#16982,1.);
#9927=VECTOR('',#16983,1.);
#9928=VECTOR('',#16986,1.);
#9929=VECTOR('',#16987,1.);
#9930=VECTOR('',#16990,1.);
#9931=VECTOR('',#16991,1.);
#9932=VECTOR('',#16998,1.);
#9933=VECTOR('',#16999,1.);
#9934=VECTOR('',#17002,1.);
#9935=VECTOR('',#17005,1.);
#9936=VECTOR('',#17008,1.);
#9937=VECTOR('',#17011,1.);
#9938=VECTOR('',#17014,1.);
#9939=VECTOR('',#17017,1.);
#9940=VECTOR('',#17020,1.);
#9941=VECTOR('',#17023,1.);
#9942=VECTOR('',#17026,1.);
#9943=VECTOR('',#17029,1.);
#9944=VECTOR('',#17032,1.);
#9945=VECTOR('',#17035,1.);
#9946=VECTOR('',#17038,1.);
#9947=VECTOR('',#17041,1.);
#9948=VECTOR('',#17044,1.);
#9949=VECTOR('',#17047,1.);
#9950=VECTOR('',#17050,1.);
#9951=VECTOR('',#17053,1.);
#9952=VECTOR('',#17056,1.);
#9953=VECTOR('',#17059,1.);
#9954=VECTOR('',#17062,1.);
#9955=VECTOR('',#17065,1.);
#9956=VECTOR('',#17068,1.);
#9957=VECTOR('',#17071,1.);
#9958=VECTOR('',#17074,1.);
#9959=VECTOR('',#17077,1.);
#9960=VECTOR('',#17080,1.);
#9961=VECTOR('',#17083,1.);
#9962=VECTOR('',#17086,1.);
#9963=VECTOR('',#17089,1.);
#9964=VECTOR('',#17092,1.);
#9965=VECTOR('',#17095,1.);
#9966=VECTOR('',#17098,1.);
#9967=VECTOR('',#17101,1.);
#9968=VECTOR('',#17104,1.);
#9969=VECTOR('',#17107,1.);
#9970=VECTOR('',#17110,1.);
#9971=VECTOR('',#17113,1.);
#9972=VECTOR('',#17116,1.);
#9973=VECTOR('',#17119,1.);
#9974=VECTOR('',#17122,1.);
#9975=VECTOR('',#17125,1.);
#9976=VECTOR('',#17128,1.);
#9977=VECTOR('',#17131,1.);
#9978=VECTOR('',#17134,1.);
#9979=VECTOR('',#17137,1.);
#9980=VECTOR('',#17140,1.);
#9981=VECTOR('',#17143,1.);
#9982=VECTOR('',#17146,1.);
#9983=VECTOR('',#17149,1.);
#9984=VECTOR('',#17152,1.);
#9985=VECTOR('',#17155,1.);
#9986=VECTOR('',#17158,1.);
#9987=VECTOR('',#17161,1.);
#9988=VECTOR('',#17164,1.);
#9989=VECTOR('',#17167,1.);
#9990=VECTOR('',#17170,1.);
#9991=VECTOR('',#17173,1.);
#9992=VECTOR('',#17176,1.);
#9993=VECTOR('',#17179,1.);
#9994=VECTOR('',#17182,1.);
#9995=VECTOR('',#17185,1.);
#9996=VECTOR('',#17188,1.);
#9997=VECTOR('',#17191,1.);
#9998=VECTOR('',#17194,1.);
#9999=VECTOR('',#17197,1.);
#10000=VECTOR('',#17200,1.);
#10001=VECTOR('',#17203,1.);
#10002=VECTOR('',#17206,1.);
#10003=VECTOR('',#17209,1.);
#10004=VECTOR('',#17212,1.);
#10005=VECTOR('',#17215,1.);
#10006=VECTOR('',#17218,1.);
#10007=VECTOR('',#17221,1.);
#10008=VECTOR('',#17224,1.);
#10009=VECTOR('',#17227,1.);
#10010=VECTOR('',#17230,1.);
#10011=VECTOR('',#17233,1.);
#10012=VECTOR('',#17236,1.);
#10013=VECTOR('',#17239,1.);
#10014=VECTOR('',#17242,1.);
#10015=VECTOR('',#17245,1.);
#10016=VECTOR('',#17248,1.);
#10017=VECTOR('',#17251,1.);
#10018=VECTOR('',#17254,1.);
#10019=VECTOR('',#17257,1.);
#10020=VECTOR('',#17260,1.);
#10021=VECTOR('',#17263,1.);
#10022=VECTOR('',#17266,1.);
#10023=VECTOR('',#17269,1.);
#10024=VECTOR('',#17272,1.);
#10025=VECTOR('',#17275,1.);
#10026=VECTOR('',#17278,1.);
#10027=VECTOR('',#17281,1.);
#10028=VECTOR('',#17284,1.);
#10029=VECTOR('',#17287,1.);
#10030=VECTOR('',#17290,1.);
#10031=VECTOR('',#17293,1.);
#10032=VECTOR('',#17296,1.);
#10033=VECTOR('',#17299,1.);
#10034=VECTOR('',#17302,1.);
#10035=VECTOR('',#17305,1.);
#10036=VECTOR('',#17308,1.);
#10037=VECTOR('',#17311,1.);
#10038=VECTOR('',#17314,1.);
#10039=VECTOR('',#17317,1.);
#10040=VECTOR('',#17320,1.);
#10041=VECTOR('',#17323,1.);
#10042=VECTOR('',#17326,1.);
#10043=VECTOR('',#17329,1.);
#10044=VECTOR('',#17332,1.);
#10045=VECTOR('',#17335,1.);
#10046=VECTOR('',#17338,1.);
#10047=VECTOR('',#17341,1.);
#10048=VECTOR('',#17344,1.);
#10049=VECTOR('',#17347,1.);
#10050=VECTOR('',#17350,1.);
#10051=VECTOR('',#17353,1.);
#10052=VECTOR('',#17356,1.);
#10053=VECTOR('',#17359,1.);
#10054=VECTOR('',#17362,1.);
#10055=VECTOR('',#17365,1.);
#10056=VECTOR('',#17368,1.);
#10057=VECTOR('',#17371,1.);
#10058=VECTOR('',#17374,1.);
#10059=VECTOR('',#17377,1.);
#10060=VECTOR('',#17380,1.);
#10061=VECTOR('',#17383,1.);
#10062=VECTOR('',#17386,1.);
#10063=VECTOR('',#17389,1.);
#10064=VECTOR('',#17392,1.);
#10065=VECTOR('',#17395,1.);
#10066=VECTOR('',#17398,1.);
#10067=VECTOR('',#17401,1.);
#10068=VECTOR('',#17404,1.);
#10069=VECTOR('',#17407,1.);
#10070=VECTOR('',#17410,1.);
#10071=VECTOR('',#17413,1.);
#10072=VECTOR('',#17416,1.);
#10073=VECTOR('',#17419,1.);
#10074=VECTOR('',#17422,1.);
#10887=EDGE_LOOP('',(#3068));
#10888=EDGE_LOOP('',(#3069));
#10889=EDGE_LOOP('',(#3070,#3071,#3072,#3073,#3074,#3075,#3076,#3077,#3078,
#3079,#3080));
#10890=EDGE_LOOP('',(#3081,#3082,#3083,#3084,#3085,#3086,#3087,#3088,#3089,
#3090,#3091));
#10891=EDGE_LOOP('',(#3092,#3093,#3094,#3095));
#10892=EDGE_LOOP('',(#3096,#3097,#3098,#3099,#3100));
#10893=EDGE_LOOP('',(#3101,#3102,#3103,#3104));
#10894=EDGE_LOOP('',(#3105));
#10895=EDGE_LOOP('',(#3106));
#10896=EDGE_LOOP('',(#3107,#3108,#3109,#3110,#3111,#3112,#3113,#3114,#3115,
#3116,#3117,#3118,#3119,#3120,#3121,#3122,#3123,#3124,#3125,#3126,#3127,
#3128,#3129,#3130,#3131,#3132,#3133,#3134,#3135,#3136,#3137,#3138,#3139,
#3140,#3141,#3142,#3143,#3144,#3145,#3146,#3147,#3148,#3149,#3150,#3151,
#3152,#3153,#3154,#3155,#3156,#3157,#3158,#3159,#3160,#3161,#3162,#3163,
#3164,#3165,#3166,#3167,#3168,#3169,#3170,#3171,#3172,#3173,#3174,#3175,
#3176,#3177,#3178,#3179,#3180,#3181,#3182,#3183,#3184,#3185,#3186,#3187,
#3188,#3189,#3190,#3191,#3192,#3193,#3194,#3195,#3196,#3197,#3198,#3199,
#3200,#3201,#3202,#3203,#3204,#3205,#3206,#3207,#3208,#3209,#3210,#3211,
#3212,#3213,#3214,#3215,#3216,#3217,#3218,#3219,#3220,#3221,#3222,#3223,
#3224,#3225,#3226,#3227,#3228,#3229,#3230,#3231,#3232,#3233,#3234,#3235,
#3236,#3237,#3238,#3239,#3240,#3241,#3242,#3243,#3244,#3245,#3246,#3247,
#3248,#3249));
#10897=EDGE_LOOP('',(#3250));
#10898=EDGE_LOOP('',(#3251,#3252,#3253,#3254,#3255,#3256,#3257,#3258,#3259,
#3260,#3261,#3262,#3263,#3264,#3265,#3266,#3267,#3268,#3269,#3270,#3271,
#3272,#3273,#3274,#3275,#3276,#3277,#3278,#3279,#3280,#3281,#3282,#3283,
#3284,#3285,#3286,#3287,#3288,#3289,#3290,#3291,#3292,#3293,#3294,#3295,
#3296,#3297,#3298,#3299,#3300,#3301,#3302,#3303,#3304,#3305,#3306,#3307,
#3308,#3309,#3310,#3311,#3312,#3313,#3314,#3315,#3316,#3317,#3318,#3319,
#3320,#3321,#3322,#3323,#3324,#3325,#3326,#3327,#3328,#3329,#3330,#3331,
#3332,#3333,#3334,#3335,#3336,#3337,#3338,#3339,#3340,#3341,#3342,#3343,
#3344,#3345,#3346,#3347,#3348,#3349,#3350,#3351,#3352,#3353,#3354,#3355,
#3356,#3357,#3358,#3359,#3360,#3361,#3362,#3363,#3364,#3365,#3366,#3367,
#3368,#3369,#3370,#3371,#3372,#3373,#3374,#3375,#3376,#3377,#3378,#3379,
#3380,#3381,#3382,#3383,#3384,#3385,#3386,#3387,#3388,#3389,#3390,#3391,
#3392,#3393));
#10899=EDGE_LOOP('',(#3394));
#10900=EDGE_LOOP('',(#3395,#3396,#3397,#3398));
#10901=EDGE_LOOP('',(#3399,#3400,#3401,#3402));
#10902=EDGE_LOOP('',(#3403,#3404,#3405,#3406));
#10903=EDGE_LOOP('',(#3407,#3408,#3409,#3410));
#10904=EDGE_LOOP('',(#3411,#3412,#3413,#3414));
#10905=EDGE_LOOP('',(#3415,#3416,#3417,#3418));
#10906=EDGE_LOOP('',(#3419,#3420,#3421,#3422));
#10907=EDGE_LOOP('',(#3423,#3424,#3425,#3426));
#10908=EDGE_LOOP('',(#3427,#3428,#3429,#3430));
#10909=EDGE_LOOP('',(#3431,#3432,#3433,#3434));
#10910=EDGE_LOOP('',(#3435,#3436,#3437,#3438));
#10911=EDGE_LOOP('',(#3439,#3440,#3441,#3442));
#10912=EDGE_LOOP('',(#3443,#3444,#3445,#3446));
#10913=EDGE_LOOP('',(#3447,#3448,#3449,#3450));
#10914=EDGE_LOOP('',(#3451,#3452,#3453,#3454));
#10915=EDGE_LOOP('',(#3455,#3456,#3457,#3458));
#10916=EDGE_LOOP('',(#3459,#3460,#3461,#3462));
#10917=EDGE_LOOP('',(#3463,#3464,#3465,#3466));
#10918=EDGE_LOOP('',(#3467,#3468,#3469,#3470));
#10919=EDGE_LOOP('',(#3471,#3472,#3473,#3474));
#10920=EDGE_LOOP('',(#3475,#3476,#3477,#3478));
#10921=EDGE_LOOP('',(#3479,#3480,#3481,#3482));
#10922=EDGE_LOOP('',(#3483,#3484,#3485,#3486));
#10923=EDGE_LOOP('',(#3487,#3488,#3489,#3490));
#10924=EDGE_LOOP('',(#3491,#3492,#3493,#3494));
#10925=EDGE_LOOP('',(#3495,#3496,#3497,#3498));
#10926=EDGE_LOOP('',(#3499,#3500,#3501,#3502));
#10927=EDGE_LOOP('',(#3503,#3504,#3505,#3506));
#10928=EDGE_LOOP('',(#3507,#3508,#3509,#3510));
#10929=EDGE_LOOP('',(#3511,#3512,#3513,#3514));
#10930=EDGE_LOOP('',(#3515,#3516,#3517,#3518));
#10931=EDGE_LOOP('',(#3519,#3520,#3521,#3522));
#10932=EDGE_LOOP('',(#3523,#3524,#3525,#3526));
#10933=EDGE_LOOP('',(#3527,#3528,#3529,#3530));
#10934=EDGE_LOOP('',(#3531,#3532,#3533,#3534));
#10935=EDGE_LOOP('',(#3535,#3536,#3537,#3538));
#10936=EDGE_LOOP('',(#3539,#3540,#3541,#3542));
#10937=EDGE_LOOP('',(#3543,#3544,#3545,#3546));
#10938=EDGE_LOOP('',(#3547,#3548,#3549,#3550));
#10939=EDGE_LOOP('',(#3551,#3552,#3553,#3554));
#10940=EDGE_LOOP('',(#3555,#3556,#3557,#3558));
#10941=EDGE_LOOP('',(#3559,#3560,#3561,#3562));
#10942=EDGE_LOOP('',(#3563,#3564,#3565,#3566));
#10943=EDGE_LOOP('',(#3567,#3568,#3569,#3570));
#10944=EDGE_LOOP('',(#3571,#3572,#3573,#3574));
#10945=EDGE_LOOP('',(#3575,#3576,#3577,#3578));
#10946=EDGE_LOOP('',(#3579,#3580,#3581,#3582));
#10947=EDGE_LOOP('',(#3583,#3584,#3585,#3586));
#10948=EDGE_LOOP('',(#3587,#3588,#3589,#3590));
#10949=EDGE_LOOP('',(#3591,#3592,#3593,#3594));
#10950=EDGE_LOOP('',(#3595,#3596,#3597,#3598));
#10951=EDGE_LOOP('',(#3599,#3600,#3601,#3602));
#10952=EDGE_LOOP('',(#3603,#3604,#3605,#3606));
#10953=EDGE_LOOP('',(#3607,#3608,#3609,#3610));
#10954=EDGE_LOOP('',(#3611,#3612,#3613,#3614));
#10955=EDGE_LOOP('',(#3615,#3616,#3617,#3618));
#10956=EDGE_LOOP('',(#3619,#3620,#3621,#3622));
#10957=EDGE_LOOP('',(#3623,#3624,#3625,#3626));
#10958=EDGE_LOOP('',(#3627,#3628,#3629,#3630));
#10959=EDGE_LOOP('',(#3631,#3632,#3633,#3634));
#10960=EDGE_LOOP('',(#3635,#3636,#3637,#3638));
#10961=EDGE_LOOP('',(#3639,#3640,#3641,#3642));
#10962=EDGE_LOOP('',(#3643,#3644,#3645,#3646));
#10963=EDGE_LOOP('',(#3647,#3648,#3649,#3650));
#10964=EDGE_LOOP('',(#3651,#3652,#3653,#3654));
#10965=EDGE_LOOP('',(#3655,#3656,#3657,#3658));
#10966=EDGE_LOOP('',(#3659,#3660,#3661,#3662));
#10967=EDGE_LOOP('',(#3663,#3664,#3665,#3666));
#10968=EDGE_LOOP('',(#3667,#3668,#3669,#3670));
#10969=EDGE_LOOP('',(#3671,#3672,#3673,#3674));
#10970=EDGE_LOOP('',(#3675,#3676,#3677,#3678));
#10971=EDGE_LOOP('',(#3679,#3680,#3681,#3682));
#10972=EDGE_LOOP('',(#3683,#3684,#3685,#3686));
#10973=EDGE_LOOP('',(#3687,#3688,#3689,#3690));
#10974=EDGE_LOOP('',(#3691,#3692,#3693,#3694));
#10975=EDGE_LOOP('',(#3695,#3696,#3697,#3698));
#10976=EDGE_LOOP('',(#3699,#3700,#3701,#3702));
#10977=EDGE_LOOP('',(#3703,#3704,#3705,#3706));
#10978=EDGE_LOOP('',(#3707,#3708,#3709,#3710));
#10979=EDGE_LOOP('',(#3711,#3712,#3713,#3714));
#10980=EDGE_LOOP('',(#3715,#3716,#3717,#3718));
#10981=EDGE_LOOP('',(#3719,#3720,#3721,#3722));
#10982=EDGE_LOOP('',(#3723,#3724,#3725,#3726));
#10983=EDGE_LOOP('',(#3727,#3728,#3729,#3730));
#10984=EDGE_LOOP('',(#3731,#3732,#3733,#3734));
#10985=EDGE_LOOP('',(#3735,#3736,#3737,#3738));
#10986=EDGE_LOOP('',(#3739,#3740,#3741,#3742));
#10987=EDGE_LOOP('',(#3743,#3744,#3745,#3746));
#10988=EDGE_LOOP('',(#3747,#3748,#3749,#3750));
#10989=EDGE_LOOP('',(#3751,#3752,#3753,#3754));
#10990=EDGE_LOOP('',(#3755,#3756,#3757,#3758));
#10991=EDGE_LOOP('',(#3759,#3760,#3761,#3762));
#10992=EDGE_LOOP('',(#3763,#3764,#3765,#3766));
#10993=EDGE_LOOP('',(#3767,#3768,#3769,#3770));
#10994=EDGE_LOOP('',(#3771,#3772,#3773,#3774));
#10995=EDGE_LOOP('',(#3775,#3776,#3777,#3778));
#10996=EDGE_LOOP('',(#3779,#3780,#3781,#3782));
#10997=EDGE_LOOP('',(#3783,#3784,#3785,#3786));
#10998=EDGE_LOOP('',(#3787,#3788,#3789,#3790));
#10999=EDGE_LOOP('',(#3791,#3792,#3793,#3794));
#11000=EDGE_LOOP('',(#3795,#3796,#3797,#3798));
#11001=EDGE_LOOP('',(#3799,#3800,#3801,#3802));
#11002=EDGE_LOOP('',(#3803,#3804,#3805,#3806));
#11003=EDGE_LOOP('',(#3807,#3808,#3809,#3810));
#11004=EDGE_LOOP('',(#3811,#3812,#3813,#3814));
#11005=EDGE_LOOP('',(#3815,#3816,#3817,#3818));
#11006=EDGE_LOOP('',(#3819,#3820,#3821,#3822));
#11007=EDGE_LOOP('',(#3823,#3824,#3825,#3826));
#11008=EDGE_LOOP('',(#3827,#3828,#3829,#3830));
#11009=EDGE_LOOP('',(#3831,#3832,#3833,#3834));
#11010=EDGE_LOOP('',(#3835,#3836,#3837,#3838));
#11011=EDGE_LOOP('',(#3839,#3840,#3841,#3842));
#11012=EDGE_LOOP('',(#3843,#3844,#3845,#3846));
#11013=EDGE_LOOP('',(#3847,#3848,#3849,#3850));
#11014=EDGE_LOOP('',(#3851,#3852,#3853,#3854));
#11015=EDGE_LOOP('',(#3855,#3856,#3857,#3858));
#11016=EDGE_LOOP('',(#3859,#3860,#3861,#3862));
#11017=EDGE_LOOP('',(#3863,#3864,#3865,#3866));
#11018=EDGE_LOOP('',(#3867,#3868,#3869,#3870));
#11019=EDGE_LOOP('',(#3871,#3872,#3873,#3874));
#11020=EDGE_LOOP('',(#3875,#3876,#3877,#3878));
#11021=EDGE_LOOP('',(#3879,#3880,#3881,#3882));
#11022=EDGE_LOOP('',(#3883,#3884,#3885,#3886));
#11023=EDGE_LOOP('',(#3887,#3888,#3889,#3890));
#11024=EDGE_LOOP('',(#3891,#3892,#3893,#3894));
#11025=EDGE_LOOP('',(#3895,#3896,#3897,#3898));
#11026=EDGE_LOOP('',(#3899,#3900,#3901,#3902));
#11027=EDGE_LOOP('',(#3903,#3904,#3905,#3906));
#11028=EDGE_LOOP('',(#3907,#3908,#3909,#3910));
#11029=EDGE_LOOP('',(#3911,#3912,#3913,#3914));
#11030=EDGE_LOOP('',(#3915,#3916,#3917,#3918));
#11031=EDGE_LOOP('',(#3919,#3920,#3921,#3922));
#11032=EDGE_LOOP('',(#3923,#3924,#3925,#3926));
#11033=EDGE_LOOP('',(#3927,#3928,#3929,#3930));
#11034=EDGE_LOOP('',(#3931,#3932,#3933,#3934));
#11035=EDGE_LOOP('',(#3935,#3936,#3937,#3938));
#11036=EDGE_LOOP('',(#3939,#3940,#3941,#3942));
#11037=EDGE_LOOP('',(#3943,#3944,#3945,#3946));
#11038=EDGE_LOOP('',(#3947,#3948,#3949,#3950));
#11039=EDGE_LOOP('',(#3951,#3952,#3953,#3954));
#11040=EDGE_LOOP('',(#3955,#3956,#3957,#3958));
#11041=EDGE_LOOP('',(#3959,#3960,#3961,#3962));
#11042=EDGE_LOOP('',(#3963,#3964,#3965,#3966));
#11043=EDGE_LOOP('',(#3967,#3968,#3969));
#11044=EDGE_LOOP('',(#3970));
#11045=EDGE_LOOP('',(#3971,#3972,#3973,#3974,#3975,#3976,#3977,#3978,#3979,
#3980,#3981,#3982,#3983,#3984,#3985,#3986,#3987,#3988,#3989));
#11046=EDGE_LOOP('',(#3990));
#11047=EDGE_LOOP('',(#3991));
#11048=EDGE_LOOP('',(#3992));
#11049=EDGE_LOOP('',(#3993));
#11050=EDGE_LOOP('',(#3994));
#11051=EDGE_LOOP('',(#3995));
#11052=EDGE_LOOP('',(#3996));
#11053=EDGE_LOOP('',(#3997));
#11054=EDGE_LOOP('',(#3998));
#11055=EDGE_LOOP('',(#3999));
#12004=FACE_BOUND('',#10887,.T.);
#12005=FACE_BOUND('',#10888,.T.);
#12006=FACE_BOUND('',#10889,.T.);
#12007=FACE_BOUND('',#10890,.T.);
#12008=FACE_BOUND('',#10891,.T.);
#12009=FACE_BOUND('',#10892,.T.);
#12010=FACE_BOUND('',#10893,.T.);
#12011=FACE_BOUND('',#10894,.T.);
#12012=FACE_BOUND('',#10895,.T.);
#12013=FACE_BOUND('',#10896,.T.);
#12014=FACE_BOUND('',#10897,.T.);
#12015=FACE_BOUND('',#10898,.T.);
#12016=FACE_BOUND('',#10899,.T.);
#12017=FACE_BOUND('',#10900,.T.);
#12018=FACE_BOUND('',#10901,.T.);
#12019=FACE_BOUND('',#10902,.T.);
#12020=FACE_BOUND('',#10903,.T.);
#12021=FACE_BOUND('',#10904,.T.);
#12022=FACE_BOUND('',#10905,.T.);
#12023=FACE_BOUND('',#10906,.T.);
#12024=FACE_BOUND('',#10907,.T.);
#12025=FACE_BOUND('',#10908,.T.);
#12026=FACE_BOUND('',#10909,.T.);
#12027=FACE_BOUND('',#10910,.T.);
#12028=FACE_BOUND('',#10911,.T.);
#12029=FACE_BOUND('',#10912,.T.);
#12030=FACE_BOUND('',#10913,.T.);
#12031=FACE_BOUND('',#10914,.T.);
#12032=FACE_BOUND('',#10915,.T.);
#12033=FACE_BOUND('',#10916,.T.);
#12034=FACE_BOUND('',#10917,.T.);
#12035=FACE_BOUND('',#10918,.T.);
#12036=FACE_BOUND('',#10919,.T.);
#12037=FACE_BOUND('',#10920,.T.);
#12038=FACE_BOUND('',#10921,.T.);
#12039=FACE_BOUND('',#10922,.T.);
#12040=FACE_BOUND('',#10923,.T.);
#12041=FACE_BOUND('',#10924,.T.);
#12042=FACE_BOUND('',#10925,.T.);
#12043=FACE_BOUND('',#10926,.T.);
#12044=FACE_BOUND('',#10927,.T.);
#12045=FACE_BOUND('',#10928,.T.);
#12046=FACE_BOUND('',#10929,.T.);
#12047=FACE_BOUND('',#10930,.T.);
#12048=FACE_BOUND('',#10931,.T.);
#12049=FACE_BOUND('',#10932,.T.);
#12050=FACE_BOUND('',#10933,.T.);
#12051=FACE_BOUND('',#10934,.T.);
#12052=FACE_BOUND('',#10935,.T.);
#12053=FACE_BOUND('',#10936,.T.);
#12054=FACE_BOUND('',#10937,.T.);
#12055=FACE_BOUND('',#10938,.T.);
#12056=FACE_BOUND('',#10939,.T.);
#12057=FACE_BOUND('',#10940,.T.);
#12058=FACE_BOUND('',#10941,.T.);
#12059=FACE_BOUND('',#10942,.T.);
#12060=FACE_BOUND('',#10943,.T.);
#12061=FACE_BOUND('',#10944,.T.);
#12062=FACE_BOUND('',#10945,.T.);
#12063=FACE_BOUND('',#10946,.T.);
#12064=FACE_BOUND('',#10947,.T.);
#12065=FACE_BOUND('',#10948,.T.);
#12066=FACE_BOUND('',#10949,.T.);
#12067=FACE_BOUND('',#10950,.T.);
#12068=FACE_BOUND('',#10951,.T.);
#12069=FACE_BOUND('',#10952,.T.);
#12070=FACE_BOUND('',#10953,.T.);
#12071=FACE_BOUND('',#10954,.T.);
#12072=FACE_BOUND('',#10955,.T.);
#12073=FACE_BOUND('',#10956,.T.);
#12074=FACE_BOUND('',#10957,.T.);
#12075=FACE_BOUND('',#10958,.T.);
#12076=FACE_BOUND('',#10959,.T.);
#12077=FACE_BOUND('',#10960,.T.);
#12078=FACE_BOUND('',#10961,.T.);
#12079=FACE_BOUND('',#10962,.T.);
#12080=FACE_BOUND('',#10963,.T.);
#12081=FACE_BOUND('',#10964,.T.);
#12082=FACE_BOUND('',#10965,.T.);
#12083=FACE_BOUND('',#10966,.T.);
#12084=FACE_BOUND('',#10967,.T.);
#12085=FACE_BOUND('',#10968,.T.);
#12086=FACE_BOUND('',#10969,.T.);
#12087=FACE_BOUND('',#10970,.T.);
#12088=FACE_BOUND('',#10971,.T.);
#12089=FACE_BOUND('',#10972,.T.);
#12090=FACE_BOUND('',#10973,.T.);
#12091=FACE_BOUND('',#10974,.T.);
#12092=FACE_BOUND('',#10975,.T.);
#12093=FACE_BOUND('',#10976,.T.);
#12094=FACE_BOUND('',#10977,.T.);
#12095=FACE_BOUND('',#10978,.T.);
#12096=FACE_BOUND('',#10979,.T.);
#12097=FACE_BOUND('',#10980,.T.);
#12098=FACE_BOUND('',#10981,.T.);
#12099=FACE_BOUND('',#10982,.T.);
#12100=FACE_BOUND('',#10983,.T.);
#12101=FACE_BOUND('',#10984,.T.);
#12102=FACE_BOUND('',#10985,.T.);
#12103=FACE_BOUND('',#10986,.T.);
#12104=FACE_BOUND('',#10987,.T.);
#12105=FACE_BOUND('',#10988,.T.);
#12106=FACE_BOUND('',#10989,.T.);
#12107=FACE_BOUND('',#10990,.T.);
#12108=FACE_BOUND('',#10991,.T.);
#12109=FACE_BOUND('',#10992,.T.);
#12110=FACE_BOUND('',#10993,.T.);
#12111=FACE_BOUND('',#10994,.T.);
#12112=FACE_BOUND('',#10995,.T.);
#12113=FACE_BOUND('',#10996,.T.);
#12114=FACE_BOUND('',#10997,.T.);
#12115=FACE_BOUND('',#10998,.T.);
#12116=FACE_BOUND('',#10999,.T.);
#12117=FACE_BOUND('',#11000,.T.);
#12118=FACE_BOUND('',#11001,.T.);
#12119=FACE_BOUND('',#11002,.T.);
#12120=FACE_BOUND('',#11003,.T.);
#12121=FACE_BOUND('',#11004,.T.);
#12122=FACE_BOUND('',#11005,.T.);
#12123=FACE_BOUND('',#11006,.T.);
#12124=FACE_BOUND('',#11007,.T.);
#12125=FACE_BOUND('',#11008,.T.);
#12126=FACE_BOUND('',#11009,.T.);
#12127=FACE_BOUND('',#11010,.T.);
#12128=FACE_BOUND('',#11011,.T.);
#12129=FACE_BOUND('',#11012,.T.);
#12130=FACE_BOUND('',#11013,.T.);
#12131=FACE_BOUND('',#11014,.T.);
#12132=FACE_BOUND('',#11015,.T.);
#12133=FACE_BOUND('',#11016,.T.);
#12134=FACE_BOUND('',#11017,.T.);
#12135=FACE_BOUND('',#11018,.T.);
#12136=FACE_BOUND('',#11019,.T.);
#12137=FACE_BOUND('',#11020,.T.);
#12138=FACE_BOUND('',#11021,.T.);
#12139=FACE_BOUND('',#11022,.T.);
#12140=FACE_BOUND('',#11023,.T.);
#12141=FACE_BOUND('',#11024,.T.);
#12142=FACE_BOUND('',#11025,.T.);
#12143=FACE_BOUND('',#11026,.T.);
#12144=FACE_BOUND('',#11027,.T.);
#12145=FACE_BOUND('',#11028,.T.);
#12146=FACE_BOUND('',#11029,.T.);
#12147=FACE_BOUND('',#11030,.T.);
#12148=FACE_BOUND('',#11031,.T.);
#12149=FACE_BOUND('',#11032,.T.);
#12150=FACE_BOUND('',#11033,.T.);
#12151=FACE_BOUND('',#11034,.T.);
#12152=FACE_BOUND('',#11035,.T.);
#12153=FACE_BOUND('',#11036,.T.);
#12154=FACE_BOUND('',#11037,.T.);
#12155=FACE_BOUND('',#11038,.T.);
#12156=FACE_BOUND('',#11039,.T.);
#12157=FACE_BOUND('',#11040,.T.);
#12158=FACE_BOUND('',#11041,.T.);
#12159=FACE_BOUND('',#11042,.T.);
#12160=FACE_BOUND('',#11043,.T.);
#12161=FACE_BOUND('',#11044,.T.);
#12162=FACE_BOUND('',#11045,.T.);
#12163=FACE_BOUND('',#11046,.T.);
#12164=FACE_BOUND('',#11047,.T.);
#12165=FACE_BOUND('',#11048,.T.);
#12166=FACE_BOUND('',#11049,.T.);
#12167=FACE_BOUND('',#11050,.T.);
#12168=FACE_BOUND('',#11051,.T.);
#12169=FACE_BOUND('',#11052,.T.);
#12170=FACE_BOUND('',#11053,.T.);
#12171=FACE_BOUND('',#11054,.T.);
#12172=FACE_BOUND('',#11055,.T.);
#12684=(
BOUNDED_SURFACE()
B_SPLINE_SURFACE(1,2,((#33568,#33569,#33570,#33571,#33572,#33573,#33574,
#33575,#33576,#33577,#33578,#33579,#33580,#33581,#33582,#33583,#33584,#33585,
#33586,#33587,#33588,#33589,#33590,#33591,#33592,#33593,#33594,#33595,#33596,
#33597,#33598,#33599,#33600,#33601,#33602,#33603,#33604,#33605,#33606,#33607,
#33608,#33609,#33610,#33611,#33612,#33613,#33614,#33615,#33616,#33617,#33618,
#33619,#33620,#33621,#33622,#33623,#33624),(#33625,#33626,#33627,#33628,
#33629,#33630,#33631,#33632,#33633,#33634,#33635,#33636,#33637,#33638,#33639,
#33640,#33641,#33642,#33643,#33644,#33645,#33646,#33647,#33648,#33649,#33650,
#33651,#33652,#33653,#33654,#33655,#33656,#33657,#33658,#33659,#33660,#33661,
#33662,#33663,#33664,#33665,#33666,#33667,#33668,#33669,#33670,#33671,#33672,
#33673,#33674,#33675,#33676,#33677,#33678,#33679,#33680,#33681)),
 .RULED_SURF.,.F.,.F.,.F.)
B_SPLINE_SURFACE_WITH_KNOTS((2,2),(3,2,2,2,2,2,2,2,2,2,2,2,2,2,2,2,2,2,
2,2,2,2,2,2,2,2,2,2,3),(0.,1.),(0.,0.03125,0.0625,0.09375,0.125,0.15625,
0.1875,0.21875,0.25,0.28125,0.3125,0.34375,0.375,0.40625,0.4375,0.46875,
0.5,0.53125,0.5625,0.59375,0.625,0.65625,0.6875,0.71875,0.75,0.78125,0.8125,
0.84375,0.875),.UNSPECIFIED.)
GEOMETRIC_REPRESENTATION_ITEM()
RATIONAL_B_SPLINE_SURFACE(((1.,0.923879532511287,1.,0.923879532511287,1.,
0.923879532511287,1.,0.923879532511287,1.,0.923879532511287,1.,0.923879532511287,
1.,0.923879532511287,1.,0.923879532511287,1.,0.923879532511287,1.,0.923879532511287,
1.,0.923879532511287,1.,0.923879532511287,1.,0.923879532511287,1.,0.923879532511287,
1.,0.923879532511287,1.,0.923879532511287,1.,0.923879532511287,1.,0.923879532511287,
1.,0.923879532511287,1.,0.923879532511287,1.,0.923879532511287,1.,0.923879532511287,
1.,0.923879532511287,1.,0.923879532511287,1.,0.923879532511287,1.,0.923879532511287,
1.,0.923879532511287,1.,0.923879532511287,1.),(1.,0.923879532511287,1.,
0.923879532511287,1.,0.923879532511287,1.,0.923879532511287,1.,0.923879532511287,
1.,0.923879532511287,1.,0.923879532511287,1.,0.923879532511287,1.,0.923879532511287,
1.,0.923879532511287,1.,0.923879532511287,1.,0.923879532511287,1.,0.923879532511287,
1.,0.923879532511287,1.,0.923879532511287,1.,0.923879532511287,1.,0.923879532511287,
1.,0.923879532511287,1.,0.923879532511287,1.,0.923879532511287,1.,0.923879532511287,
1.,0.923879532511287,1.,0.923879532511287,1.,0.923879532511287,1.,0.923879532511287,
1.,0.923879532511287,1.,0.923879532511287,1.,0.923879532511287,1.)))
REPRESENTATION_ITEM('')
SURFACE()
);
#12685=(
BOUNDED_SURFACE()
B_SPLINE_SURFACE(1,2,((#33816,#33817,#33818,#33819,#33820,#33821,#33822,
#33823,#33824,#33825,#33826,#33827,#33828,#33829,#33830,#33831,#33832,#33833,
#33834,#33835,#33836,#33837,#33838,#33839,#33840,#33841,#33842,#33843,#33844,
#33845,#33846,#33847,#33848,#33849,#33850,#33851,#33852,#33853,#33854,#33855,
#33856,#33857,#33858,#33859,#33860,#33861,#33862,#33863,#33864,#33865,#33866,
#33867,#33868,#33869,#33870,#33871,#33872),(#33873,#33874,#33875,#33876,
#33877,#33878,#33879,#33880,#33881,#33882,#33883,#33884,#33885,#33886,#33887,
#33888,#33889,#33890,#33891,#33892,#33893,#33894,#33895,#33896,#33897,#33898,
#33899,#33900,#33901,#33902,#33903,#33904,#33905,#33906,#33907,#33908,#33909,
#33910,#33911,#33912,#33913,#33914,#33915,#33916,#33917,#33918,#33919,#33920,
#33921,#33922,#33923,#33924,#33925,#33926,#33927,#33928,#33929)),
 .RULED_SURF.,.F.,.F.,.F.)
B_SPLINE_SURFACE_WITH_KNOTS((2,2),(3,2,2,2,2,2,2,2,2,2,2,2,2,2,2,2,2,2,
2,2,2,2,2,2,2,2,2,2,3),(0.,1.),(0.,0.03125,0.0625,0.09375,0.125,0.15625,
0.1875,0.21875,0.25,0.28125,0.3125,0.34375,0.375,0.40625,0.4375,0.46875,
0.5,0.53125,0.5625,0.59375,0.625,0.65625,0.6875,0.71875,0.75,0.78125,0.8125,
0.84375,0.875),.UNSPECIFIED.)
GEOMETRIC_REPRESENTATION_ITEM()
RATIONAL_B_SPLINE_SURFACE(((1.,0.923879532511287,1.,0.923879532511287,1.,
0.923879532511287,1.,0.923879532511287,1.,0.923879532511287,1.,0.923879532511287,
1.,0.923879532511287,1.,0.923879532511287,1.,0.923879532511287,1.,0.923879532511287,
1.,0.923879532511287,1.,0.923879532511287,1.,0.923879532511287,1.,0.923879532511287,
1.,0.923879532511287,1.,0.923879532511287,1.,0.923879532511287,1.,0.923879532511287,
1.,0.923879532511287,1.,0.923879532511287,1.,0.923879532511287,1.,0.923879532511287,
1.,0.923879532511287,1.,0.923879532511287,1.,0.923879532511287,1.,0.923879532511287,
1.,0.923879532511287,1.,0.923879532511287,1.),(1.,0.923879532511287,1.,
0.923879532511287,1.,0.923879532511287,1.,0.923879532511287,1.,0.923879532511287,
1.,0.923879532511287,1.,0.923879532511287,1.,0.923879532511287,1.,0.923879532511287,
1.,0.923879532511287,1.,0.923879532511287,1.,0.923879532511287,1.,0.923879532511287,
1.,0.923879532511287,1.,0.923879532511287,1.,0.923879532511287,1.,0.923879532511287,
1.,0.923879532511287,1.,0.923879532511287,1.,0.923879532511287,1.,0.923879532511287,
1.,0.923879532511287,1.,0.923879532511287,1.,0.923879532511287,1.,0.923879532511287,
1.,0.923879532511287,1.,0.923879532511287,1.,0.923879532511287,1.)))
REPRESENTATION_ITEM('')
SURFACE()
);
#13000=ADVANCED_FACE('',(#12004,#12005),#15,.F.);
#13001=ADVANCED_FACE('',(#12006),#12684,.F.);
#13002=ADVANCED_FACE('',(#12007),#12685,.F.);
#13003=ADVANCED_FACE('',(#12008),#1637,.T.);
#13004=ADVANCED_FACE('',(#12009),#1290,.T.);
#13005=ADVANCED_FACE('',(#12010),#1291,.T.);
#13006=ADVANCED_FACE('',(#12011,#12012),#1292,.T.);
#13007=ADVANCED_FACE('',(#12013,#12014),#1293,.F.);
#13008=ADVANCED_FACE('',(#12015,#12016),#1294,.T.);
#13009=ADVANCED_FACE('',(#12017),#1638,.T.);
#13010=ADVANCED_FACE('',(#12018),#1295,.F.);
#13011=ADVANCED_FACE('',(#12019),#1296,.F.);
#13012=ADVANCED_FACE('',(#12020),#1639,.T.);
#13013=ADVANCED_FACE('',(#12021),#1297,.F.);
#13014=ADVANCED_FACE('',(#12022),#1298,.F.);
#13015=ADVANCED_FACE('',(#12023),#1640,.T.);
#13016=ADVANCED_FACE('',(#12024),#1299,.F.);
#13017=ADVANCED_FACE('',(#12025),#1300,.F.);
#13018=ADVANCED_FACE('',(#12026),#1641,.T.);
#13019=ADVANCED_FACE('',(#12027),#1301,.F.);
#13020=ADVANCED_FACE('',(#12028),#1302,.F.);
#13021=ADVANCED_FACE('',(#12029),#1642,.T.);
#13022=ADVANCED_FACE('',(#12030),#1303,.F.);
#13023=ADVANCED_FACE('',(#12031),#1304,.F.);
#13024=ADVANCED_FACE('',(#12032),#1643,.T.);
#13025=ADVANCED_FACE('',(#12033),#1305,.F.);
#13026=ADVANCED_FACE('',(#12034),#1306,.F.);
#13027=ADVANCED_FACE('',(#12035),#1644,.T.);
#13028=ADVANCED_FACE('',(#12036),#1307,.F.);
#13029=ADVANCED_FACE('',(#12037),#1308,.F.);
#13030=ADVANCED_FACE('',(#12038),#1645,.T.);
#13031=ADVANCED_FACE('',(#12039),#1309,.F.);
#13032=ADVANCED_FACE('',(#12040),#1310,.F.);
#13033=ADVANCED_FACE('',(#12041),#1646,.T.);
#13034=ADVANCED_FACE('',(#12042),#1311,.F.);
#13035=ADVANCED_FACE('',(#12043),#1312,.F.);
#13036=ADVANCED_FACE('',(#12044),#1647,.T.);
#13037=ADVANCED_FACE('',(#12045),#1313,.F.);
#13038=ADVANCED_FACE('',(#12046),#1314,.F.);
#13039=ADVANCED_FACE('',(#12047),#1648,.T.);
#13040=ADVANCED_FACE('',(#12048),#1315,.F.);
#13041=ADVANCED_FACE('',(#12049),#1316,.F.);
#13042=ADVANCED_FACE('',(#12050),#1649,.T.);
#13043=ADVANCED_FACE('',(#12051),#1317,.F.);
#13044=ADVANCED_FACE('',(#12052),#1318,.F.);
#13045=ADVANCED_FACE('',(#12053),#1650,.T.);
#13046=ADVANCED_FACE('',(#12054),#1319,.F.);
#13047=ADVANCED_FACE('',(#12055),#1320,.F.);
#13048=ADVANCED_FACE('',(#12056),#1651,.T.);
#13049=ADVANCED_FACE('',(#12057),#1321,.F.);
#13050=ADVANCED_FACE('',(#12058),#1322,.F.);
#13051=ADVANCED_FACE('',(#12059),#1652,.T.);
#13052=ADVANCED_FACE('',(#12060),#1323,.F.);
#13053=ADVANCED_FACE('',(#12061),#1324,.F.);
#13054=ADVANCED_FACE('',(#12062),#1653,.T.);
#13055=ADVANCED_FACE('',(#12063),#1325,.F.);
#13056=ADVANCED_FACE('',(#12064),#1326,.F.);
#13057=ADVANCED_FACE('',(#12065),#1654,.T.);
#13058=ADVANCED_FACE('',(#12066),#1327,.F.);
#13059=ADVANCED_FACE('',(#12067),#1328,.F.);
#13060=ADVANCED_FACE('',(#12068),#1655,.T.);
#13061=ADVANCED_FACE('',(#12069),#1329,.F.);
#13062=ADVANCED_FACE('',(#12070),#1330,.F.);
#13063=ADVANCED_FACE('',(#12071),#1656,.T.);
#13064=ADVANCED_FACE('',(#12072),#1331,.F.);
#13065=ADVANCED_FACE('',(#12073),#1332,.F.);
#13066=ADVANCED_FACE('',(#12074),#1657,.T.);
#13067=ADVANCED_FACE('',(#12075),#1333,.F.);
#13068=ADVANCED_FACE('',(#12076),#1334,.F.);
#13069=ADVANCED_FACE('',(#12077),#1658,.T.);
#13070=ADVANCED_FACE('',(#12078),#1335,.F.);
#13071=ADVANCED_FACE('',(#12079),#1336,.F.);
#13072=ADVANCED_FACE('',(#12080),#1659,.T.);
#13073=ADVANCED_FACE('',(#12081),#1337,.F.);
#13074=ADVANCED_FACE('',(#12082),#1338,.F.);
#13075=ADVANCED_FACE('',(#12083),#1660,.T.);
#13076=ADVANCED_FACE('',(#12084),#1339,.F.);
#13077=ADVANCED_FACE('',(#12085),#1340,.F.);
#13078=ADVANCED_FACE('',(#12086),#1661,.T.);
#13079=ADVANCED_FACE('',(#12087),#1341,.F.);
#13080=ADVANCED_FACE('',(#12088),#1342,.F.);
#13081=ADVANCED_FACE('',(#12089),#1662,.T.);
#13082=ADVANCED_FACE('',(#12090),#1343,.F.);
#13083=ADVANCED_FACE('',(#12091),#1344,.F.);
#13084=ADVANCED_FACE('',(#12092),#1663,.T.);
#13085=ADVANCED_FACE('',(#12093),#1345,.F.);
#13086=ADVANCED_FACE('',(#12094),#1346,.F.);
#13087=ADVANCED_FACE('',(#12095),#1664,.T.);
#13088=ADVANCED_FACE('',(#12096),#1347,.F.);
#13089=ADVANCED_FACE('',(#12097),#1348,.F.);
#13090=ADVANCED_FACE('',(#12098),#1665,.T.);
#13091=ADVANCED_FACE('',(#12099),#1349,.F.);
#13092=ADVANCED_FACE('',(#12100),#1350,.F.);
#13093=ADVANCED_FACE('',(#12101),#1666,.T.);
#13094=ADVANCED_FACE('',(#12102),#1351,.F.);
#13095=ADVANCED_FACE('',(#12103),#1352,.F.);
#13096=ADVANCED_FACE('',(#12104),#1667,.T.);
#13097=ADVANCED_FACE('',(#12105),#1353,.F.);
#13098=ADVANCED_FACE('',(#12106),#1354,.F.);
#13099=ADVANCED_FACE('',(#12107),#1668,.T.);
#13100=ADVANCED_FACE('',(#12108),#1355,.F.);
#13101=ADVANCED_FACE('',(#12109),#1356,.F.);
#13102=ADVANCED_FACE('',(#12110),#1669,.T.);
#13103=ADVANCED_FACE('',(#12111),#1357,.F.);
#13104=ADVANCED_FACE('',(#12112),#1358,.F.);
#13105=ADVANCED_FACE('',(#12113),#1670,.T.);
#13106=ADVANCED_FACE('',(#12114),#1359,.F.);
#13107=ADVANCED_FACE('',(#12115),#1360,.F.);
#13108=ADVANCED_FACE('',(#12116),#1671,.T.);
#13109=ADVANCED_FACE('',(#12117),#1361,.F.);
#13110=ADVANCED_FACE('',(#12118),#1362,.F.);
#13111=ADVANCED_FACE('',(#12119),#1672,.T.);
#13112=ADVANCED_FACE('',(#12120),#1363,.F.);
#13113=ADVANCED_FACE('',(#12121),#1364,.F.);
#13114=ADVANCED_FACE('',(#12122),#1673,.T.);
#13115=ADVANCED_FACE('',(#12123),#1365,.F.);
#13116=ADVANCED_FACE('',(#12124),#1366,.F.);
#13117=ADVANCED_FACE('',(#12125),#1674,.T.);
#13118=ADVANCED_FACE('',(#12126),#1367,.F.);
#13119=ADVANCED_FACE('',(#12127),#1368,.F.);
#13120=ADVANCED_FACE('',(#12128),#1675,.T.);
#13121=ADVANCED_FACE('',(#12129),#1369,.F.);
#13122=ADVANCED_FACE('',(#12130),#1370,.F.);
#13123=ADVANCED_FACE('',(#12131),#1676,.T.);
#13124=ADVANCED_FACE('',(#12132),#1371,.F.);
#13125=ADVANCED_FACE('',(#12133),#1372,.F.);
#13126=ADVANCED_FACE('',(#12134),#1677,.T.);
#13127=ADVANCED_FACE('',(#12135),#1373,.F.);
#13128=ADVANCED_FACE('',(#12136),#1374,.F.);
#13129=ADVANCED_FACE('',(#12137),#1678,.T.);
#13130=ADVANCED_FACE('',(#12138),#1375,.F.);
#13131=ADVANCED_FACE('',(#12139),#1376,.F.);
#13132=ADVANCED_FACE('',(#12140),#1679,.T.);
#13133=ADVANCED_FACE('',(#12141),#1377,.F.);
#13134=ADVANCED_FACE('',(#12142),#1378,.F.);
#13135=ADVANCED_FACE('',(#12143),#1680,.T.);
#13136=ADVANCED_FACE('',(#12144),#1379,.F.);
#13137=ADVANCED_FACE('',(#12145),#1380,.F.);
#13138=ADVANCED_FACE('',(#12146),#1381,.F.);
#13139=ADVANCED_FACE('',(#12147),#1382,.F.);
#13140=ADVANCED_FACE('',(#12148),#1681,.T.);
#13141=ADVANCED_FACE('',(#12149),#1383,.F.);
#13142=ADVANCED_FACE('',(#12150),#1384,.F.);
#13143=ADVANCED_FACE('',(#12151),#1682,.T.);
#13144=ADVANCED_FACE('',(#12152),#1385,.F.);
#13145=ADVANCED_FACE('',(#12153),#1386,.F.);
#13146=ADVANCED_FACE('',(#12154),#1683,.T.);
#13147=ADVANCED_FACE('',(#12155),#1387,.F.);
#13148=ADVANCED_FACE('',(#12156),#1388,.F.);
#13149=ADVANCED_FACE('',(#12157),#1684,.T.);
#13150=ADVANCED_FACE('',(#12158),#1389,.F.);
#13151=ADVANCED_FACE('',(#12159),#1390,.F.);
#13152=ADVANCED_FACE('',(#12160,#12161),#1391,.T.);
#13153=ADVANCED_FACE('',(#12162),#1685,.T.);
#13154=ADVANCED_FACE('',(#12163,#12164),#1686,.T.);
#13155=ADVANCED_FACE('',(#12165,#12166),#1687,.F.);
#13156=ADVANCED_FACE('',(#12167,#12168),#1688,.F.);
#13157=ADVANCED_FACE('',(#12169,#12170),#315,.T.);
#13158=ADVANCED_FACE('',(#12171,#12172),#316,.T.);
#13513=CLOSED_SHELL('',(#13000,#13001,#13002,#13003,#13004,#13005,#13006,
#13007,#13008,#13009,#13010,#13011,#13012,#13013,#13014,#13015,#13016,#13017,
#13018,#13019,#13020,#13021,#13022,#13023,#13024,#13025,#13026,#13027,#13028,
#13029,#13030,#13031,#13032,#13033,#13034,#13035,#13036,#13037,#13038,#13039,
#13040,#13041,#13042,#13043,#13044,#13045,#13046,#13047,#13048,#13049,#13050,
#13051,#13052,#13053,#13054,#13055,#13056,#13057,#13058,#13059,#13060,#13061,
#13062,#13063,#13064,#13065,#13066,#13067,#13068,#13069,#13070,#13071,#13072,
#13073,#13074,#13075,#13076,#13077,#13078,#13079,#13080,#13081,#13082,#13083,
#13084,#13085,#13086,#13087,#13088,#13089,#13090,#13091,#13092,#13093,#13094,
#13095,#13096,#13097,#13098,#13099,#13100,#13101,#13102,#13103,#13104,#13105,
#13106,#13107,#13108,#13109,#13110,#13111,#13112,#13113,#13114,#13115,#13116,
#13117,#13118,#13119,#13120,#13121,#13122,#13123,#13124,#13125,#13126,#13127,
#13128,#13129,#13130,#13131,#13132,#13133,#13134,#13135,#13136,#13137,#13138,
#13139,#13140,#13141,#13142,#13143,#13144,#13145,#13146,#13147,#13148,#13149,
#13150,#13151,#13152,#13153,#13154,#13155,#13156,#13157,#13158));
#13540=STYLED_ITEM('',(#13567),#13730);
#13567=PRESENTATION_STYLE_ASSIGNMENT((#13594));
#13594=SURFACE_STYLE_USAGE(.BOTH.,#13621);
#13621=SURFACE_SIDE_STYLE('',(#13648));
#13648=SURFACE_STYLE_FILL_AREA(#13675);
#13675=FILL_AREA_STYLE('',(#13702));
#13702=FILL_AREA_STYLE_COLOUR('',#63);
#13730=MANIFOLD_SOLID_BREP('Nozzle cap',#13513);
#13758=SHAPE_DEFINITION_REPRESENTATION(#45548,#13786);
#13786=SHAPE_REPRESENTATION('Nozzle cap',(#13802),#45476);
#13802=AXIS2_PLACEMENT_3D('',#19109,#15295,#15296);
#14380=AXIS2_PLACEMENT_3D('',#33563,#16581,#16582);
#14381=AXIS2_PLACEMENT_3D('',#33564,#16583,#16584);
#14382=AXIS2_PLACEMENT_3D('',#33566,#16585,#16586);
#14383=AXIS2_PLACEMENT_3D('',#34064,#16591,#16592);
#14384=AXIS2_PLACEMENT_3D('',#34067,#16595,#16596);
#14385=AXIS2_PLACEMENT_3D('',#34071,#16599,#16600);
#14386=AXIS2_PLACEMENT_3D('',#34073,#16602,#16603);
#14387=AXIS2_PLACEMENT_3D('',#34074,#16604,#16605);
#14388=AXIS2_PLACEMENT_3D('',#34075,#16606,#16607);
#14389=AXIS2_PLACEMENT_3D('',#34077,#16608,#16609);
#14390=AXIS2_PLACEMENT_3D('',#34081,#16611,#16612);
#14391=AXIS2_PLACEMENT_3D('',#34087,#16615,#16616);
#14392=AXIS2_PLACEMENT_3D('',#34093,#16619,#16620);
#14393=AXIS2_PLACEMENT_3D('',#34099,#16623,#16624);
#14394=AXIS2_PLACEMENT_3D('',#34105,#16627,#16628);
#14395=AXIS2_PLACEMENT_3D('',#34111,#16631,#16632);
#14396=AXIS2_PLACEMENT_3D('',#34117,#16635,#16636);
#14397=AXIS2_PLACEMENT_3D('',#34123,#16639,#16640);
#14398=AXIS2_PLACEMENT_3D('',#34129,#16643,#16644);
#14399=AXIS2_PLACEMENT_3D('',#34135,#16647,#16648);
#14400=AXIS2_PLACEMENT_3D('',#34141,#16651,#16652);
#14401=AXIS2_PLACEMENT_3D('',#34147,#16655,#16656);
#14402=AXIS2_PLACEMENT_3D('',#34153,#16659,#16660);
#14403=AXIS2_PLACEMENT_3D('',#34159,#16663,#16664);
#14404=AXIS2_PLACEMENT_3D('',#34165,#16667,#16668);
#14405=AXIS2_PLACEMENT_3D('',#34171,#16671,#16672);
#14406=AXIS2_PLACEMENT_3D('',#34177,#16675,#16676);
#14407=AXIS2_PLACEMENT_3D('',#34183,#16679,#16680);
#14408=AXIS2_PLACEMENT_3D('',#34189,#16683,#16684);
#14409=AXIS2_PLACEMENT_3D('',#34195,#16687,#16688);
#14410=AXIS2_PLACEMENT_3D('',#34201,#16691,#16692);
#14411=AXIS2_PLACEMENT_3D('',#34207,#16695,#16696);
#14412=AXIS2_PLACEMENT_3D('',#34213,#16699,#16700);
#14413=AXIS2_PLACEMENT_3D('',#34219,#16703,#16704);
#14414=AXIS2_PLACEMENT_3D('',#34225,#16707,#16708);
#14415=AXIS2_PLACEMENT_3D('',#34231,#16711,#16712);
#14416=AXIS2_PLACEMENT_3D('',#34237,#16715,#16716);
#14417=AXIS2_PLACEMENT_3D('',#34243,#16719,#16720);
#14418=AXIS2_PLACEMENT_3D('',#34249,#16723,#16724);
#14419=AXIS2_PLACEMENT_3D('',#34255,#16727,#16728);
#14420=AXIS2_PLACEMENT_3D('',#34261,#16731,#16732);
#14421=AXIS2_PLACEMENT_3D('',#34267,#16735,#16736);
#14422=AXIS2_PLACEMENT_3D('',#34273,#16739,#16740);
#14423=AXIS2_PLACEMENT_3D('',#34279,#16743,#16744);
#14424=AXIS2_PLACEMENT_3D('',#34285,#16747,#16748);
#14425=AXIS2_PLACEMENT_3D('',#34291,#16751,#16752);
#14426=AXIS2_PLACEMENT_3D('',#34297,#16755,#16756);
#14427=AXIS2_PLACEMENT_3D('',#34303,#16759,#16760);
#14428=AXIS2_PLACEMENT_3D('',#34309,#16763,#16764);
#14429=AXIS2_PLACEMENT_3D('',#34315,#16767,#16768);
#14430=AXIS2_PLACEMENT_3D('',#34321,#16771,#16772);
#14431=AXIS2_PLACEMENT_3D('',#34327,#16775,#16776);
#14432=AXIS2_PLACEMENT_3D('',#34333,#16779,#16780);
#14433=AXIS2_PLACEMENT_3D('',#34343,#16785,#16786);
#14434=AXIS2_PLACEMENT_3D('',#34349,#16789,#16790);
#14435=AXIS2_PLACEMENT_3D('',#34355,#16793,#16794);
#14436=AXIS2_PLACEMENT_3D('',#34361,#16797,#16798);
#14437=AXIS2_PLACEMENT_3D('',#34364,#16800,#16801);
#14438=AXIS2_PLACEMENT_3D('',#34366,#16802,#16803);
#14439=AXIS2_PLACEMENT_3D('',#34372,#16806,#16807);
#14440=AXIS2_PLACEMENT_3D('',#34378,#16810,#16811);
#14441=AXIS2_PLACEMENT_3D('',#34384,#16814,#16815);
#14442=AXIS2_PLACEMENT_3D('',#34390,#16818,#16819);
#14443=AXIS2_PLACEMENT_3D('',#34400,#16824,#16825);
#14444=AXIS2_PLACEMENT_3D('',#34406,#16828,#16829);
#14445=AXIS2_PLACEMENT_3D('',#34412,#16832,#16833);
#14446=AXIS2_PLACEMENT_3D('',#34418,#16836,#16837);
#14447=AXIS2_PLACEMENT_3D('',#34424,#16840,#16841);
#14448=AXIS2_PLACEMENT_3D('',#34430,#16844,#16845);
#14449=AXIS2_PLACEMENT_3D('',#34436,#16848,#16849);
#14450=AXIS2_PLACEMENT_3D('',#34442,#16852,#16853);
#14451=AXIS2_PLACEMENT_3D('',#34448,#16856,#16857);
#14452=AXIS2_PLACEMENT_3D('',#34454,#16860,#16861);
#14453=AXIS2_PLACEMENT_3D('',#34460,#16864,#16865);
#14454=AXIS2_PLACEMENT_3D('',#34466,#16868,#16869);
#14455=AXIS2_PLACEMENT_3D('',#34472,#16872,#16873);
#14456=AXIS2_PLACEMENT_3D('',#34478,#16876,#16877);
#14457=AXIS2_PLACEMENT_3D('',#34484,#16880,#16881);
#14458=AXIS2_PLACEMENT_3D('',#34490,#16884,#16885);
#14459=AXIS2_PLACEMENT_3D('',#34496,#16888,#16889);
#14460=AXIS2_PLACEMENT_3D('',#34502,#16892,#16893);
#14461=AXIS2_PLACEMENT_3D('',#34508,#16896,#16897);
#14462=AXIS2_PLACEMENT_3D('',#34514,#16900,#16901);
#14463=AXIS2_PLACEMENT_3D('',#34520,#16904,#16905);
#14464=AXIS2_PLACEMENT_3D('',#34526,#16908,#16909);
#14465=AXIS2_PLACEMENT_3D('',#34532,#16912,#16913);
#14466=AXIS2_PLACEMENT_3D('',#34538,#16916,#16917);
#14467=AXIS2_PLACEMENT_3D('',#34544,#16920,#16921);
#14468=AXIS2_PLACEMENT_3D('',#34550,#16924,#16925);
#14469=AXIS2_PLACEMENT_3D('',#34556,#16928,#16929);
#14470=AXIS2_PLACEMENT_3D('',#34562,#16932,#16933);
#14471=AXIS2_PLACEMENT_3D('',#34568,#16936,#16937);
#14472=AXIS2_PLACEMENT_3D('',#34574,#16940,#16941);
#14473=AXIS2_PLACEMENT_3D('',#34580,#16944,#16945);
#14474=AXIS2_PLACEMENT_3D('',#34586,#16948,#16949);
#14475=AXIS2_PLACEMENT_3D('',#34592,#16952,#16953);
#14476=AXIS2_PLACEMENT_3D('',#34598,#16956,#16957);
#14477=AXIS2_PLACEMENT_3D('',#34604,#16960,#16961);
#14478=AXIS2_PLACEMENT_3D('',#34610,#16964,#16965);
#14479=AXIS2_PLACEMENT_3D('',#34616,#16968,#16969);
#14480=AXIS2_PLACEMENT_3D('',#34622,#16972,#16973);
#14481=AXIS2_PLACEMENT_3D('',#34628,#16976,#16977);
#14482=AXIS2_PLACEMENT_3D('',#34634,#16980,#16981);
#14483=AXIS2_PLACEMENT_3D('',#34640,#16984,#16985);
#14484=AXIS2_PLACEMENT_3D('',#34646,#16988,#16989);
#14485=AXIS2_PLACEMENT_3D('',#34652,#16992,#16993);
#14486=AXIS2_PLACEMENT_3D('',#34653,#16994,#16995);
#14487=AXIS2_PLACEMENT_3D('',#34655,#16996,#16997);
#14488=AXIS2_PLACEMENT_3D('',#34658,#17000,#17001);
#14489=AXIS2_PLACEMENT_3D('',#34660,#17003,#17004);
#14490=AXIS2_PLACEMENT_3D('',#34662,#17006,#17007);
#14491=AXIS2_PLACEMENT_3D('',#34664,#17009,#17010);
#14492=AXIS2_PLACEMENT_3D('',#34666,#17012,#17013);
#14493=AXIS2_PLACEMENT_3D('',#34668,#17015,#17016);
#14494=AXIS2_PLACEMENT_3D('',#34670,#17018,#17019);
#14495=AXIS2_PLACEMENT_3D('',#34672,#17021,#17022);
#14496=AXIS2_PLACEMENT_3D('',#34674,#17024,#17025);
#14497=AXIS2_PLACEMENT_3D('',#34676,#17027,#17028);
#14498=AXIS2_PLACEMENT_3D('',#34678,#17030,#17031);
#14499=AXIS2_PLACEMENT_3D('',#34680,#17033,#17034);
#14500=AXIS2_PLACEMENT_3D('',#34682,#17036,#17037);
#14501=AXIS2_PLACEMENT_3D('',#34684,#17039,#17040);
#14502=AXIS2_PLACEMENT_3D('',#34686,#17042,#17043);
#14503=AXIS2_PLACEMENT_3D('',#34688,#17045,#17046);
#14504=AXIS2_PLACEMENT_3D('',#34690,#17048,#17049);
#14505=AXIS2_PLACEMENT_3D('',#34692,#17051,#17052);
#14506=AXIS2_PLACEMENT_3D('',#34694,#17054,#17055);
#14507=AXIS2_PLACEMENT_3D('',#34696,#17057,#17058);
#14508=AXIS2_PLACEMENT_3D('',#34698,#17060,#17061);
#14509=AXIS2_PLACEMENT_3D('',#34700,#17063,#17064);
#14510=AXIS2_PLACEMENT_3D('',#34702,#17066,#17067);
#14511=AXIS2_PLACEMENT_3D('',#34704,#17069,#17070);
#14512=AXIS2_PLACEMENT_3D('',#34706,#17072,#17073);
#14513=AXIS2_PLACEMENT_3D('',#34708,#17075,#17076);
#14514=AXIS2_PLACEMENT_3D('',#34710,#17078,#17079);
#14515=AXIS2_PLACEMENT_3D('',#34712,#17081,#17082);
#14516=AXIS2_PLACEMENT_3D('',#34714,#17084,#17085);
#14517=AXIS2_PLACEMENT_3D('',#34716,#17087,#17088);
#14518=AXIS2_PLACEMENT_3D('',#34718,#17090,#17091);
#14519=AXIS2_PLACEMENT_3D('',#34720,#17093,#17094);
#14520=AXIS2_PLACEMENT_3D('',#34722,#17096,#17097);
#14521=AXIS2_PLACEMENT_3D('',#34724,#17099,#17100);
#14522=AXIS2_PLACEMENT_3D('',#34726,#17102,#17103);
#14523=AXIS2_PLACEMENT_3D('',#34728,#17105,#17106);
#14524=AXIS2_PLACEMENT_3D('',#34730,#17108,#17109);
#14525=AXIS2_PLACEMENT_3D('',#34732,#17111,#17112);
#14526=AXIS2_PLACEMENT_3D('',#34734,#17114,#17115);
#14527=AXIS2_PLACEMENT_3D('',#34736,#17117,#17118);
#14528=AXIS2_PLACEMENT_3D('',#34738,#17120,#17121);
#14529=AXIS2_PLACEMENT_3D('',#34740,#17123,#17124);
#14530=AXIS2_PLACEMENT_3D('',#34742,#17126,#17127);
#14531=AXIS2_PLACEMENT_3D('',#34744,#17129,#17130);
#14532=AXIS2_PLACEMENT_3D('',#34746,#17132,#17133);
#14533=AXIS2_PLACEMENT_3D('',#34748,#17135,#17136);
#14534=AXIS2_PLACEMENT_3D('',#34750,#17138,#17139);
#14535=AXIS2_PLACEMENT_3D('',#34752,#17141,#17142);
#14536=AXIS2_PLACEMENT_3D('',#34754,#17144,#17145);
#14537=AXIS2_PLACEMENT_3D('',#34756,#17147,#17148);
#14538=AXIS2_PLACEMENT_3D('',#34758,#17150,#17151);
#14539=AXIS2_PLACEMENT_3D('',#34760,#17153,#17154);
#14540=AXIS2_PLACEMENT_3D('',#34762,#17156,#17157);
#14541=AXIS2_PLACEMENT_3D('',#34764,#17159,#17160);
#14542=AXIS2_PLACEMENT_3D('',#34766,#17162,#17163);
#14543=AXIS2_PLACEMENT_3D('',#34768,#17165,#17166);
#14544=AXIS2_PLACEMENT_3D('',#34770,#17168,#17169);
#14545=AXIS2_PLACEMENT_3D('',#34772,#17171,#17172);
#14546=AXIS2_PLACEMENT_3D('',#34774,#17174,#17175);
#14547=AXIS2_PLACEMENT_3D('',#34776,#17177,#17178);
#14548=AXIS2_PLACEMENT_3D('',#34778,#17180,#17181);
#14549=AXIS2_PLACEMENT_3D('',#34780,#17183,#17184);
#14550=AXIS2_PLACEMENT_3D('',#34782,#17186,#17187);
#14551=AXIS2_PLACEMENT_3D('',#34784,#17189,#17190);
#14552=AXIS2_PLACEMENT_3D('',#34786,#17192,#17193);
#14553=AXIS2_PLACEMENT_3D('',#34788,#17195,#17196);
#14554=AXIS2_PLACEMENT_3D('',#34790,#17198,#17199);
#14555=AXIS2_PLACEMENT_3D('',#34792,#17201,#17202);
#14556=AXIS2_PLACEMENT_3D('',#34794,#17204,#17205);
#14557=AXIS2_PLACEMENT_3D('',#34796,#17207,#17208);
#14558=AXIS2_PLACEMENT_3D('',#34798,#17210,#17211);
#14559=AXIS2_PLACEMENT_3D('',#34800,#17213,#17214);
#14560=AXIS2_PLACEMENT_3D('',#34802,#17216,#17217);
#14561=AXIS2_PLACEMENT_3D('',#34804,#17219,#17220);
#14562=AXIS2_PLACEMENT_3D('',#34806,#17222,#17223);
#14563=AXIS2_PLACEMENT_3D('',#34808,#17225,#17226);
#14564=AXIS2_PLACEMENT_3D('',#34810,#17228,#17229);
#14565=AXIS2_PLACEMENT_3D('',#34812,#17231,#17232);
#14566=AXIS2_PLACEMENT_3D('',#34814,#17234,#17235);
#14567=AXIS2_PLACEMENT_3D('',#34816,#17237,#17238);
#14568=AXIS2_PLACEMENT_3D('',#34818,#17240,#17241);
#14569=AXIS2_PLACEMENT_3D('',#34820,#17243,#17244);
#14570=AXIS2_PLACEMENT_3D('',#34822,#17246,#17247);
#14571=AXIS2_PLACEMENT_3D('',#34824,#17249,#17250);
#14572=AXIS2_PLACEMENT_3D('',#34826,#17252,#17253);
#14573=AXIS2_PLACEMENT_3D('',#34828,#17255,#17256);
#14574=AXIS2_PLACEMENT_3D('',#34830,#17258,#17259);
#14575=AXIS2_PLACEMENT_3D('',#34832,#17261,#17262);
#14576=AXIS2_PLACEMENT_3D('',#34834,#17264,#17265);
#14577=AXIS2_PLACEMENT_3D('',#34836,#17267,#17268);
#14578=AXIS2_PLACEMENT_3D('',#34838,#17270,#17271);
#14579=AXIS2_PLACEMENT_3D('',#34840,#17273,#17274);
#14580=AXIS2_PLACEMENT_3D('',#34842,#17276,#17277);
#14581=AXIS2_PLACEMENT_3D('',#34844,#17279,#17280);
#14582=AXIS2_PLACEMENT_3D('',#34846,#17282,#17283);
#14583=AXIS2_PLACEMENT_3D('',#34848,#17285,#17286);
#14584=AXIS2_PLACEMENT_3D('',#34850,#17288,#17289);
#14585=AXIS2_PLACEMENT_3D('',#34852,#17291,#17292);
#14586=AXIS2_PLACEMENT_3D('',#34854,#17294,#17295);
#14587=AXIS2_PLACEMENT_3D('',#34856,#17297,#17298);
#14588=AXIS2_PLACEMENT_3D('',#34858,#17300,#17301);
#14589=AXIS2_PLACEMENT_3D('',#34860,#17303,#17304);
#14590=AXIS2_PLACEMENT_3D('',#34862,#17306,#17307);
#14591=AXIS2_PLACEMENT_3D('',#34864,#17309,#17310);
#14592=AXIS2_PLACEMENT_3D('',#34866,#17312,#17313);
#14593=AXIS2_PLACEMENT_3D('',#34868,#17315,#17316);
#14594=AXIS2_PLACEMENT_3D('',#34870,#17318,#17319);
#14595=AXIS2_PLACEMENT_3D('',#34872,#17321,#17322);
#14596=AXIS2_PLACEMENT_3D('',#34874,#17324,#17325);
#14597=AXIS2_PLACEMENT_3D('',#34876,#17327,#17328);
#14598=AXIS2_PLACEMENT_3D('',#34878,#17330,#17331);
#14599=AXIS2_PLACEMENT_3D('',#34880,#17333,#17334);
#14600=AXIS2_PLACEMENT_3D('',#34882,#17336,#17337);
#14601=AXIS2_PLACEMENT_3D('',#34884,#17339,#17340);
#14602=AXIS2_PLACEMENT_3D('',#34886,#17342,#17343);
#14603=AXIS2_PLACEMENT_3D('',#34888,#17345,#17346);
#14604=AXIS2_PLACEMENT_3D('',#34890,#17348,#17349);
#14605=AXIS2_PLACEMENT_3D('',#34892,#17351,#17352);
#14606=AXIS2_PLACEMENT_3D('',#34894,#17354,#17355);
#14607=AXIS2_PLACEMENT_3D('',#34896,#17357,#17358);
#14608=AXIS2_PLACEMENT_3D('',#34898,#17360,#17361);
#14609=AXIS2_PLACEMENT_3D('',#34900,#17363,#17364);
#14610=AXIS2_PLACEMENT_3D('',#34902,#17366,#17367);
#14611=AXIS2_PLACEMENT_3D('',#34904,#17369,#17370);
#14612=AXIS2_PLACEMENT_3D('',#34906,#17372,#17373);
#14613=AXIS2_PLACEMENT_3D('',#34908,#17375,#17376);
#14614=AXIS2_PLACEMENT_3D('',#34910,#17378,#17379);
#14615=AXIS2_PLACEMENT_3D('',#34912,#17381,#17382);
#14616=AXIS2_PLACEMENT_3D('',#34914,#17384,#17385);
#14617=AXIS2_PLACEMENT_3D('',#34916,#17387,#17388);
#14618=AXIS2_PLACEMENT_3D('',#34918,#17390,#17391);
#14619=AXIS2_PLACEMENT_3D('',#34920,#17393,#17394);
#14620=AXIS2_PLACEMENT_3D('',#34922,#17396,#17397);
#14621=AXIS2_PLACEMENT_3D('',#34924,#17399,#17400);
#14622=AXIS2_PLACEMENT_3D('',#34926,#17402,#17403);
#14623=AXIS2_PLACEMENT_3D('',#34928,#17405,#17406);
#14624=AXIS2_PLACEMENT_3D('',#34930,#17408,#17409);
#14625=AXIS2_PLACEMENT_3D('',#34932,#17411,#17412);
#14626=AXIS2_PLACEMENT_3D('',#34934,#17414,#17415);
#14627=AXIS2_PLACEMENT_3D('',#34936,#17417,#17418);
#14628=AXIS2_PLACEMENT_3D('',#34938,#17420,#17421);
#14629=AXIS2_PLACEMENT_3D('',#34940,#17423,#17424);
#14630=AXIS2_PLACEMENT_3D('',#34941,#17425,#17426);
#14631=AXIS2_PLACEMENT_3D('',#34942,#17427,#17428);
#14632=AXIS2_PLACEMENT_3D('',#34943,#17429,#17430);
#14633=AXIS2_PLACEMENT_3D('',#34945,#17431,#17432);
#14634=AXIS2_PLACEMENT_3D('',#34946,#17433,#17434);
#14635=AXIS2_PLACEMENT_3D('',#34947,#17435,#17436);
#14636=AXIS2_PLACEMENT_3D('',#34948,#17437,#17438);
#14637=AXIS2_PLACEMENT_3D('',#34950,#17439,#17440);
#14638=AXIS2_PLACEMENT_3D('',#34951,#17441,#17442);
#14639=AXIS2_PLACEMENT_3D('',#34953,#17443,#17444);
#14640=AXIS2_PLACEMENT_3D('',#34954,#17445,#17446);
#15295=DIRECTION('',(0.,0.,1.));
#15296=DIRECTION('',(1.,0.,0.));
#16581=DIRECTION('',(0.,1.,0.));
#16582=DIRECTION('',(1.,0.,0.));
#16583=DIRECTION('',(0.,-1.,0.));
#16584=DIRECTION('',(0.,0.,-1.));
#16585=DIRECTION('',(0.,1.,0.));
#16586=DIRECTION('',(0.,0.,-1.));
#16587=DIRECTION('',(0.86602540378444,-0.5,0.));
#16588=DIRECTION('',(0.866025403784438,0.5,-1.06057523872491E-16));
#16589=DIRECTION('',(-0.86602540378444,-0.5,0.));
#16590=DIRECTION('',(-0.86602540378444,0.5,1.06057523872491E-16));
#16591=DIRECTION('',(0.,1.,0.));
#16592=DIRECTION('',(0.,0.,1.));
#16593=DIRECTION('',(0.,-1.,0.));
#16594=DIRECTION('',(0.,1.,0.));
#16595=DIRECTION('',(0.,0.,1.));
#16596=DIRECTION('',(1.,0.,0.));
#16597=DIRECTION('',(-1.,0.,1.22464679914735E-16));
#16598=DIRECTION('',(0.,-1.,0.));
#16599=DIRECTION('',(0.,0.,1.));
#16600=DIRECTION('',(1.,0.,0.));
#16601=DIRECTION('',(0.,1.,0.));
#16602=DIRECTION('',(0.,1.,0.));
#16603=DIRECTION('',(0.,0.,1.));
#16604=DIRECTION('',(0.,1.,0.));
#16605=DIRECTION('',(0.,0.,1.));
#16606=DIRECTION('',(0.,-1.,0.));
#16607=DIRECTION('',(0.,0.,1.));
#16608=DIRECTION('',(0.,1.,0.));
#16609=DIRECTION('',(0.,0.,1.));
#16610=DIRECTION('',(0.86602540378444,0.,-0.5));
#16611=DIRECTION('',(0.,1.,0.));
#16612=DIRECTION('',(0.,0.,1.));
#16613=DIRECTION('',(-0.793353340291235,0.,-0.608761429008721));
#16614=DIRECTION('',(0.923879532511287,0.,-0.382683432365091));
#16615=DIRECTION('',(0.,1.,0.));
#16616=DIRECTION('',(0.,0.,1.));
#16617=DIRECTION('',(-0.707106781186548,0.,-0.707106781186548));
#16618=DIRECTION('',(0.965925826289068,0.,-0.258819045102522));
#16619=DIRECTION('',(0.,1.,0.));
#16620=DIRECTION('',(0.,0.,1.));
#16621=DIRECTION('',(-0.60876142900872,0.,-0.793353340291235));
#16622=DIRECTION('',(0.99144486137381,0.,-0.130526192220053));
#16623=DIRECTION('',(0.,1.,0.));
#16624=DIRECTION('',(0.,0.,1.));
#16625=DIRECTION('',(-0.5,0.,-0.866025403784439));
#16626=DIRECTION('',(1.,0.,-1.47392777911416E-15));
#16627=DIRECTION('',(0.,1.,0.));
#16628=DIRECTION('',(0.,0.,1.));
#16629=DIRECTION('',(-0.382683432365089,0.,-0.923879532511287));
#16630=DIRECTION('',(0.991444861373811,0.,0.130526192220051));
#16631=DIRECTION('',(0.,1.,0.));
#16632=DIRECTION('',(0.,0.,1.));
#16633=DIRECTION('',(-0.258819045102521,0.,-0.965925826289068));
#16634=DIRECTION('',(0.965925826289069,0.,0.25881904510252));
#16635=DIRECTION('',(0.,1.,0.));
#16636=DIRECTION('',(0.,0.,1.));
#16637=DIRECTION('',(-0.130526192220051,0.,-0.99144486137381));
#16638=DIRECTION('',(0.923879532511287,0.,0.382683432365089));
#16639=DIRECTION('',(0.,1.,0.));
#16640=DIRECTION('',(0.,0.,1.));
#16641=DIRECTION('',(7.36963889557083E-16,0.,-1.));
#16642=DIRECTION('',(0.866025403784439,0.,0.5));
#16643=DIRECTION('',(0.,1.,0.));
#16644=DIRECTION('',(0.,0.,1.));
#16645=DIRECTION('',(0.130526192220052,0.,-0.99144486137381));
#16646=DIRECTION('',(0.793353340291236,0.,0.608761429008719));
#16647=DIRECTION('',(0.,1.,0.));
#16648=DIRECTION('',(0.,0.,1.));
#16649=DIRECTION('',(0.258819045102521,0.,-0.965925826289068));
#16650=DIRECTION('',(0.707106781186549,0.,0.707106781186547));
#16651=DIRECTION('',(0.,1.,0.));
#16652=DIRECTION('',(0.,0.,1.));
#16653=DIRECTION('',(0.38268343236509,0.,-0.923879532511287));
#16654=DIRECTION('',(0.608761429008721,0.,0.793353340291235));
#16655=DIRECTION('',(0.,1.,0.));
#16656=DIRECTION('',(0.,0.,1.));
#16657=DIRECTION('',(0.5,0.,-0.866025403784439));
#16658=DIRECTION('',(0.5,0.,0.866025403784438));
#16659=DIRECTION('',(0.,1.,0.));
#16660=DIRECTION('',(0.,0.,1.));
#16661=DIRECTION('',(0.608761429008722,0.,-0.793353340291234));
#16662=DIRECTION('',(0.382683432365091,0.,0.923879532511286));
#16663=DIRECTION('',(0.,1.,0.));
#16664=DIRECTION('',(0.,0.,1.));
#16665=DIRECTION('',(0.707106781186548,0.,-0.707106781186548));
#16666=DIRECTION('',(0.258819045102522,0.,0.965925826289068));
#16667=DIRECTION('',(0.,1.,0.));
#16668=DIRECTION('',(0.,0.,1.));
#16669=DIRECTION('',(0.793353340291235,0.,-0.608761429008721));
#16670=DIRECTION('',(0.130526192220053,0.,0.99144486137381));
#16671=DIRECTION('',(0.,1.,0.));
#16672=DIRECTION('',(0.,0.,1.));
#16673=DIRECTION('',(0.866025403784439,0.,-0.5));
#16674=DIRECTION('',(1.47392777911416E-15,0.,1.));
#16675=DIRECTION('',(0.,1.,0.));
#16676=DIRECTION('',(0.,0.,1.));
#16677=DIRECTION('',(0.923879532511287,0.,-0.38268343236509));
#16678=DIRECTION('',(-0.130526192220051,0.,0.991444861373811));
#16679=DIRECTION('',(0.,1.,0.));
#16680=DIRECTION('',(0.,0.,1.));
#16681=DIRECTION('',(0.965925826289068,0.,-0.258819045102521));
#16682=DIRECTION('',(-0.258819045102519,0.,0.965925826289069));
#16683=DIRECTION('',(0.,1.,0.));
#16684=DIRECTION('',(0.,0.,1.));
#16685=DIRECTION('',(0.99144486137381,0.,-0.130526192220052));
#16686=DIRECTION('',(-0.382683432365088,0.,0.923879532511288));
#16687=DIRECTION('',(0.,1.,0.));
#16688=DIRECTION('',(0.,0.,1.));
#16689=DIRECTION('',(1.,0.,0.));
#16690=DIRECTION('',(-0.5,0.,0.86602540378444));
#16691=DIRECTION('',(0.,1.,0.));
#16692=DIRECTION('',(0.,0.,1.));
#16693=DIRECTION('',(0.99144486137381,0.,0.130526192220052));
#16694=DIRECTION('',(-0.608761429008719,0.,0.793353340291236));
#16695=DIRECTION('',(0.,1.,0.));
#16696=DIRECTION('',(0.,0.,1.));
#16697=DIRECTION('',(0.965925826289068,0.,0.258819045102521));
#16698=DIRECTION('',(-0.707106781186546,0.,0.707106781186549));
#16699=DIRECTION('',(0.,1.,0.));
#16700=DIRECTION('',(0.,0.,1.));
#16701=DIRECTION('',(0.923879532511287,0.,0.382683432365089));
#16702=DIRECTION('',(-0.793353340291235,0.,0.608761429008721));
#16703=DIRECTION('',(0.,1.,0.));
#16704=DIRECTION('',(0.,0.,1.));
#16705=DIRECTION('',(0.866025403784439,0.,0.5));
#16706=DIRECTION('',(-0.866025403784438,0.,0.5));
#16707=DIRECTION('',(0.,1.,0.));
#16708=DIRECTION('',(0.,0.,1.));
#16709=DIRECTION('',(0.793353340291235,0.,0.608761429008722));
#16710=DIRECTION('',(-0.923879532511286,0.,0.382683432365092));
#16711=DIRECTION('',(0.,1.,0.));
#16712=DIRECTION('',(0.,0.,1.));
#16713=DIRECTION('',(0.707106781186548,0.,0.707106781186547));
#16714=DIRECTION('',(-0.965925826289068,0.,0.258819045102523));
#16715=DIRECTION('',(0.,1.,0.));
#16716=DIRECTION('',(0.,0.,1.));
#16717=DIRECTION('',(0.608761429008721,0.,0.793353340291235));
#16718=DIRECTION('',(-0.99144486137381,0.,0.130526192220053));
#16719=DIRECTION('',(0.,1.,0.));
#16720=DIRECTION('',(0.,0.,1.));
#16721=DIRECTION('',(0.5,0.,0.866025403784439));
#16722=DIRECTION('',(-1.,0.,1.47392777911416E-15));
#16723=DIRECTION('',(0.,1.,0.));
#16724=DIRECTION('',(0.,0.,1.));
#16725=DIRECTION('',(0.38268343236509,0.,0.923879532511287));
#16726=DIRECTION('',(-0.991444861373811,0.,-0.130526192220051));
#16727=DIRECTION('',(0.,1.,0.));
#16728=DIRECTION('',(0.,0.,1.));
#16729=DIRECTION('',(0.258819045102521,0.,0.965925826289068));
#16730=DIRECTION('',(-0.965925826289069,0.,-0.258819045102519));
#16731=DIRECTION('',(0.,1.,0.));
#16732=DIRECTION('',(0.,0.,1.));
#16733=DIRECTION('',(0.130526192220052,0.,0.99144486137381));
#16734=DIRECTION('',(-0.923879532511288,0.,-0.382683432365088));
#16735=DIRECTION('',(0.,1.,0.));
#16736=DIRECTION('',(0.,0.,1.));
#16737=DIRECTION('',(-7.36963889557083E-16,0.,1.));
#16738=DIRECTION('',(-0.86602540378444,0.,-0.5));
#16739=DIRECTION('',(0.,1.,0.));
#16740=DIRECTION('',(0.,0.,1.));
#16741=DIRECTION('',(-0.130526192220052,0.,0.99144486137381));
#16742=DIRECTION('',(-0.793353340291236,0.,-0.608761429008719));
#16743=DIRECTION('',(0.,1.,0.));
#16744=DIRECTION('',(0.,0.,1.));
#16745=DIRECTION('',(-0.25881904510252,0.,0.965925826289068));
#16746=DIRECTION('',(-0.707106781186549,0.,-0.707106781186546));
#16747=DIRECTION('',(0.,1.,0.));
#16748=DIRECTION('',(0.,0.,1.));
#16749=DIRECTION('',(-0.38268343236509,0.,0.923879532511287));
#16750=DIRECTION('',(-0.608761429008723,0.,-0.793353340291234));
#16751=DIRECTION('',(0.,1.,0.));
#16752=DIRECTION('',(0.,0.,1.));
#16753=DIRECTION('',(-0.5,0.,0.866025403784439));
#16754=DIRECTION('',(-0.5,0.,-0.866025403784438));
#16755=DIRECTION('',(0.,1.,0.));
#16756=DIRECTION('',(0.,0.,1.));
#16757=DIRECTION('',(-0.608761429008721,0.,0.793353340291235));
#16758=DIRECTION('',(-0.382683432365092,0.,-0.923879532511286));
#16759=DIRECTION('',(0.,1.,0.));
#16760=DIRECTION('',(0.,0.,1.));
#16761=DIRECTION('',(-0.707106781186548,0.,0.707106781186548));
#16762=DIRECTION('',(-0.258819045102522,0.,-0.965925826289068));
#16763=DIRECTION('',(0.,1.,0.));
#16764=DIRECTION('',(0.,0.,1.));
#16765=DIRECTION('',(-0.793353340291235,0.,0.608761429008721));
#16766=DIRECTION('',(-0.130526192220053,0.,-0.99144486137381));
#16767=DIRECTION('',(0.,1.,0.));
#16768=DIRECTION('',(0.,0.,1.));
#16769=DIRECTION('',(-0.866025403784439,0.,0.5));
#16770=DIRECTION('',(-2.21089166867125E-15,0.,-1.));
#16771=DIRECTION('',(0.,1.,0.));
#16772=DIRECTION('',(0.,0.,1.));
#16773=DIRECTION('',(-0.923879532511287,0.,0.382683432365091));
#16774=DIRECTION('',(0.13052619222005,0.,-0.991444861373811));
#16775=DIRECTION('',(0.,1.,0.));
#16776=DIRECTION('',(0.,0.,1.));
#16777=DIRECTION('',(-0.965925826289068,0.,0.258819045102521));
#16778=DIRECTION('',(0.258819045102519,0.,-0.965925826289069));
#16779=DIRECTION('',(0.,1.,0.));
#16780=DIRECTION('',(0.,0.,1.));
#16781=DIRECTION('',(-0.99144486137381,0.,0.130526192220052));
#16782=DIRECTION('',(0.382476066482387,0.,-0.923965399010245));
#16783=DIRECTION('',(-1.,0.,-7.36963889557082E-16));
#16784=DIRECTION('',(0.5,0.,-0.866025403784439));
#16785=DIRECTION('',(0.,1.,0.));
#16786=DIRECTION('',(0.,0.,1.));
#16787=DIRECTION('',(-0.99144486137381,0.,-0.130526192220051));
#16788=DIRECTION('',(0.608761429008719,0.,-0.793353340291237));
#16789=DIRECTION('',(0.,1.,0.));
#16790=DIRECTION('',(0.,0.,1.));
#16791=DIRECTION('',(-0.965925826289068,0.,-0.258819045102521));
#16792=DIRECTION('',(0.707106781186546,0.,-0.707106781186549));
#16793=DIRECTION('',(0.,1.,0.));
#16794=DIRECTION('',(0.,0.,1.));
#16795=DIRECTION('',(-0.923879532511287,0.,-0.38268343236509));
#16796=DIRECTION('',(0.793353340291234,0.,-0.608761429008723));
#16797=DIRECTION('',(0.,1.,0.));
#16798=DIRECTION('',(0.,0.,1.));
#16799=DIRECTION('',(-0.866025403784438,0.,-0.5));
#16800=DIRECTION('',(0.,-1.,0.));
#16801=DIRECTION('',(0.,0.,-1.));
#16802=DIRECTION('',(0.,1.,0.));
#16803=DIRECTION('',(0.,0.,1.));
#16804=DIRECTION('',(0.86602540378444,0.,-0.5));
#16805=DIRECTION('',(-0.866025403784438,0.,-0.5));
#16806=DIRECTION('',(0.,1.,0.));
#16807=DIRECTION('',(0.,0.,1.));
#16808=DIRECTION('',(0.793353340291234,0.,-0.608761429008723));
#16809=DIRECTION('',(-0.923879532511287,0.,-0.38268343236509));
#16810=DIRECTION('',(0.,1.,0.));
#16811=DIRECTION('',(0.,0.,1.));
#16812=DIRECTION('',(0.707106781186546,0.,-0.707106781186549));
#16813=DIRECTION('',(-0.965925826289068,0.,-0.258819045102521));
#16814=DIRECTION('',(0.,1.,0.));
#16815=DIRECTION('',(0.,0.,1.));
#16816=DIRECTION('',(0.608761429008719,0.,-0.793353340291237));
#16817=DIRECTION('',(-0.99144486137381,0.,-0.130526192220051));
#16818=DIRECTION('',(0.,1.,0.));
#16819=DIRECTION('',(0.,0.,1.));
#16820=DIRECTION('',(0.5,0.,-0.866025403784439));
#16821=DIRECTION('',(-1.,0.,-7.36963889557082E-16));
#16822=DIRECTION('',(0.382476066482387,0.,-0.923965399010245));
#16823=DIRECTION('',(-0.99144486137381,0.,0.130526192220052));
#16824=DIRECTION('',(0.,1.,0.));
#16825=DIRECTION('',(0.,0.,1.));
#16826=DIRECTION('',(0.258819045102519,0.,-0.965925826289069));
#16827=DIRECTION('',(-0.965925826289068,0.,0.258819045102521));
#16828=DIRECTION('',(0.,1.,0.));
#16829=DIRECTION('',(0.,0.,1.));
#16830=DIRECTION('',(0.13052619222005,0.,-0.991444861373811));
#16831=DIRECTION('',(-0.923879532511287,0.,0.382683432365091));
#16832=DIRECTION('',(0.,1.,0.));
#16833=DIRECTION('',(0.,0.,1.));
#16834=DIRECTION('',(-2.21089166867125E-15,0.,-1.));
#16835=DIRECTION('',(-0.866025403784439,0.,0.5));
#16836=DIRECTION('',(0.,1.,0.));
#16837=DIRECTION('',(0.,0.,1.));
#16838=DIRECTION('',(-0.130526192220053,0.,-0.99144486137381));
#16839=DIRECTION('',(-0.793353340291235,0.,0.608761429008721));
#16840=DIRECTION('',(0.,1.,0.));
#16841=DIRECTION('',(0.,0.,1.));
#16842=DIRECTION('',(-0.258819045102522,0.,-0.965925826289068));
#16843=DIRECTION('',(-0.707106781186548,0.,0.707106781186548));
#16844=DIRECTION('',(0.,1.,0.));
#16845=DIRECTION('',(0.,0.,1.));
#16846=DIRECTION('',(-0.382683432365092,0.,-0.923879532511286));
#16847=DIRECTION('',(-0.608761429008721,0.,0.793353340291235));
#16848=DIRECTION('',(0.,1.,0.));
#16849=DIRECTION('',(0.,0.,1.));
#16850=DIRECTION('',(-0.5,0.,-0.866025403784438));
#16851=DIRECTION('',(-0.5,0.,0.866025403784439));
#16852=DIRECTION('',(0.,1.,0.));
#16853=DIRECTION('',(0.,0.,1.));
#16854=DIRECTION('',(-0.608761429008723,0.,-0.793353340291234));
#16855=DIRECTION('',(-0.38268343236509,0.,0.923879532511287));
#16856=DIRECTION('',(0.,1.,0.));
#16857=DIRECTION('',(0.,0.,1.));
#16858=DIRECTION('',(-0.707106781186549,0.,-0.707106781186546));
#16859=DIRECTION('',(-0.25881904510252,0.,0.965925826289068));
#16860=DIRECTION('',(0.,1.,0.));
#16861=DIRECTION('',(0.,0.,1.));
#16862=DIRECTION('',(-0.793353340291236,0.,-0.608761429008719));
#16863=DIRECTION('',(-0.130526192220052,0.,0.99144486137381));
#16864=DIRECTION('',(0.,1.,0.));
#16865=DIRECTION('',(0.,0.,1.));
#16866=DIRECTION('',(-0.86602540378444,0.,-0.5));
#16867=DIRECTION('',(-7.36963889557083E-16,0.,1.));
#16868=DIRECTION('',(0.,1.,0.));
#16869=DIRECTION('',(0.,0.,1.));
#16870=DIRECTION('',(-0.923879532511288,0.,-0.382683432365088));
#16871=DIRECTION('',(0.130526192220052,0.,0.99144486137381));
#16872=DIRECTION('',(0.,1.,0.));
#16873=DIRECTION('',(0.,0.,1.));
#16874=DIRECTION('',(-0.965925826289069,0.,-0.258819045102519));
#16875=DIRECTION('',(0.258819045102521,0.,0.965925826289068));
#16876=DIRECTION('',(0.,1.,0.));
#16877=DIRECTION('',(0.,0.,1.));
#16878=DIRECTION('',(-0.991444861373811,0.,-0.130526192220051));
#16879=DIRECTION('',(0.38268343236509,0.,0.923879532511287));
#16880=DIRECTION('',(0.,1.,0.));
#16881=DIRECTION('',(0.,0.,1.));
#16882=DIRECTION('',(-1.,0.,1.47392777911416E-15));
#16883=DIRECTION('',(0.5,0.,0.866025403784439));
#16884=DIRECTION('',(0.,1.,0.));
#16885=DIRECTION('',(0.,0.,1.));
#16886=DIRECTION('',(-0.99144486137381,0.,0.130526192220053));
#16887=DIRECTION('',(0.608761429008721,0.,0.793353340291235));
#16888=DIRECTION('',(0.,1.,0.));
#16889=DIRECTION('',(0.,0.,1.));
#16890=DIRECTION('',(-0.965925826289068,0.,0.258819045102523));
#16891=DIRECTION('',(0.707106781186548,0.,0.707106781186547));
#16892=DIRECTION('',(0.,1.,0.));
#16893=DIRECTION('',(0.,0.,1.));
#16894=DIRECTION('',(-0.923879532511286,0.,0.382683432365092));
#16895=DIRECTION('',(0.793353340291235,0.,0.608761429008722));
#16896=DIRECTION('',(0.,1.,0.));
#16897=DIRECTION('',(0.,0.,1.));
#16898=DIRECTION('',(-0.866025403784438,0.,0.5));
#16899=DIRECTION('',(0.866025403784439,0.,0.5));
#16900=DIRECTION('',(0.,1.,0.));
#16901=DIRECTION('',(0.,0.,1.));
#16902=DIRECTION('',(-0.793353340291235,0.,0.608761429008721));
#16903=DIRECTION('',(0.923879532511287,0.,0.382683432365089));
#16904=DIRECTION('',(0.,1.,0.));
#16905=DIRECTION('',(0.,0.,1.));
#16906=DIRECTION('',(-0.707106781186546,0.,0.707106781186549));
#16907=DIRECTION('',(0.965925826289068,0.,0.258819045102521));
#16908=DIRECTION('',(0.,1.,0.));
#16909=DIRECTION('',(0.,0.,1.));
#16910=DIRECTION('',(-0.608761429008719,0.,0.793353340291236));
#16911=DIRECTION('',(0.99144486137381,0.,0.130526192220052));
#16912=DIRECTION('',(0.,1.,0.));
#16913=DIRECTION('',(0.,0.,1.));
#16914=DIRECTION('',(-0.5,0.,0.86602540378444));
#16915=DIRECTION('',(1.,0.,0.));
#16916=DIRECTION('',(0.,1.,0.));
#16917=DIRECTION('',(0.,0.,1.));
#16918=DIRECTION('',(-0.382683432365088,0.,0.923879532511288));
#16919=DIRECTION('',(0.99144486137381,0.,-0.130526192220052));
#16920=DIRECTION('',(0.,1.,0.));
#16921=DIRECTION('',(0.,0.,1.));
#16922=DIRECTION('',(-0.258819045102519,0.,0.965925826289069));
#16923=DIRECTION('',(0.965925826289068,0.,-0.258819045102521));
#16924=DIRECTION('',(0.,1.,0.));
#16925=DIRECTION('',(0.,0.,1.));
#16926=DIRECTION('',(-0.130526192220051,0.,0.991444861373811));
#16927=DIRECTION('',(0.923879532511287,0.,-0.38268343236509));
#16928=DIRECTION('',(0.,1.,0.));
#16929=DIRECTION('',(0.,0.,1.));
#16930=DIRECTION('',(1.47392777911416E-15,0.,1.));
#16931=DIRECTION('',(0.866025403784439,0.,-0.5));
#16932=DIRECTION('',(0.,1.,0.));
#16933=DIRECTION('',(0.,0.,1.));
#16934=DIRECTION('',(0.130526192220053,0.,0.99144486137381));
#16935=DIRECTION('',(0.793353340291235,0.,-0.608761429008721));
#16936=DIRECTION('',(0.,1.,0.));
#16937=DIRECTION('',(0.,0.,1.));
#16938=DIRECTION('',(0.258819045102522,0.,0.965925826289068));
#16939=DIRECTION('',(0.707106781186548,0.,-0.707106781186548));
#16940=DIRECTION('',(0.,1.,0.));
#16941=DIRECTION('',(0.,0.,1.));
#16942=DIRECTION('',(0.382683432365091,0.,0.923879532511286));
#16943=DIRECTION('',(0.608761429008722,0.,-0.793353340291234));
#16944=DIRECTION('',(0.,1.,0.));
#16945=DIRECTION('',(0.,0.,1.));
#16946=DIRECTION('',(0.5,0.,0.866025403784438));
#16947=DIRECTION('',(0.5,0.,-0.866025403784439));
#16948=DIRECTION('',(0.,1.,0.));
#16949=DIRECTION('',(0.,0.,1.));
#16950=DIRECTION('',(0.608761429008721,0.,0.793353340291235));
#16951=DIRECTION('',(0.38268343236509,0.,-0.923879532511287));
#16952=DIRECTION('',(0.,1.,0.));
#16953=DIRECTION('',(0.,0.,1.));
#16954=DIRECTION('',(0.707106781186549,0.,0.707106781186547));
#16955=DIRECTION('',(0.258819045102521,0.,-0.965925826289068));
#16956=DIRECTION('',(0.,1.,0.));
#16957=DIRECTION('',(0.,0.,1.));
#16958=DIRECTION('',(0.793353340291236,0.,0.608761429008719));
#16959=DIRECTION('',(0.130526192220052,0.,-0.99144486137381));
#16960=DIRECTION('',(0.,1.,0.));
#16961=DIRECTION('',(0.,0.,1.));
#16962=DIRECTION('',(0.866025403784439,0.,0.5));
#16963=DIRECTION('',(7.36963889557083E-16,0.,-1.));
#16964=DIRECTION('',(0.,1.,0.));
#16965=DIRECTION('',(0.,0.,1.));
#16966=DIRECTION('',(0.923879532511287,0.,0.382683432365089));
#16967=DIRECTION('',(-0.130526192220051,0.,-0.99144486137381));
#16968=DIRECTION('',(0.,1.,0.));
#16969=DIRECTION('',(0.,0.,1.));
#16970=DIRECTION('',(0.965925826289069,0.,0.25881904510252));
#16971=DIRECTION('',(-0.258819045102521,0.,-0.965925826289068));
#16972=DIRECTION('',(0.,1.,0.));
#16973=DIRECTION('',(0.,0.,1.));
#16974=DIRECTION('',(0.991444861373811,0.,0.130526192220051));
#16975=DIRECTION('',(-0.382683432365089,0.,-0.923879532511287));
#16976=DIRECTION('',(0.,1.,0.));
#16977=DIRECTION('',(0.,0.,1.));
#16978=DIRECTION('',(1.,0.,-1.47392777911416E-15));
#16979=DIRECTION('',(-0.5,0.,-0.866025403784439));
#16980=DIRECTION('',(0.,1.,0.));
#16981=DIRECTION('',(0.,0.,1.));
#16982=DIRECTION('',(0.99144486137381,0.,-0.130526192220053));
#16983=DIRECTION('',(-0.60876142900872,0.,-0.793353340291235));
#16984=DIRECTION('',(0.,1.,0.));
#16985=DIRECTION('',(0.,0.,1.));
#16986=DIRECTION('',(0.965925826289068,0.,-0.258819045102522));
#16987=DIRECTION('',(-0.707106781186548,0.,-0.707106781186548));
#16988=DIRECTION('',(0.,1.,0.));
#16989=DIRECTION('',(0.,0.,1.));
#16990=DIRECTION('',(0.923879532511287,0.,-0.382683432365091));
#16991=DIRECTION('',(-0.793353340291235,0.,-0.608761429008721));
#16992=DIRECTION('',(0.,1.,0.));
#16993=DIRECTION('',(0.,0.,1.));
#16994=DIRECTION('',(0.,1.,0.));
#16995=DIRECTION('',(0.,0.,1.));
#16996=DIRECTION('',(0.,-1.,0.));
#16997=DIRECTION('',(0.,0.,-1.));
#16998=DIRECTION('',(0.,-1.,0.));
#16999=DIRECTION('',(0.,-1.,0.));
#17000=DIRECTION('',(-0.608761429008719,0.,0.793353340291236));
#17001=DIRECTION('',(0.793353340291236,0.,0.608761429008719));
#17002=DIRECTION('',(0.,-1.,0.));
#17003=DIRECTION('',(-0.38268343236509,0.,-0.923879532511287));
#17004=DIRECTION('',(-0.923879532511287,0.,0.38268343236509));
#17005=DIRECTION('',(0.,-1.,0.));
#17006=DIRECTION('',(0.,-1.,0.));
#17007=DIRECTION('',(0.,0.,-1.));
#17008=DIRECTION('',(0.,-1.,0.));
#17009=DIRECTION('',(-0.707106781186548,0.,0.707106781186548));
#17010=DIRECTION('',(0.707106781186548,0.,0.707106781186548));
#17011=DIRECTION('',(0.,-1.,0.));
#17012=DIRECTION('',(-0.258819045102521,0.,-0.965925826289068));
#17013=DIRECTION('',(-0.965925826289068,0.,0.258819045102521));
#17014=DIRECTION('',(0.,-1.,0.));
#17015=DIRECTION('',(0.,-1.,0.));
#17016=DIRECTION('',(0.,0.,-1.));
#17017=DIRECTION('',(0.,-1.,0.));
#17018=DIRECTION('',(-0.793353340291234,0.,0.608761429008723));
#17019=DIRECTION('',(0.608761429008723,0.,0.793353340291234));
#17020=DIRECTION('',(0.,-1.,0.));
#17021=DIRECTION('',(-0.130526192220052,0.,-0.99144486137381));
#17022=DIRECTION('',(-0.99144486137381,0.,0.130526192220052));
#17023=DIRECTION('',(0.,-1.,0.));
#17024=DIRECTION('',(0.,-1.,0.));
#17025=DIRECTION('',(0.,0.,-1.));
#17026=DIRECTION('',(0.,-1.,0.));
#17027=DIRECTION('',(-0.866025403784438,0.,0.5));
#17028=DIRECTION('',(0.5,0.,0.866025403784438));
#17029=DIRECTION('',(0.,-1.,0.));
#17030=DIRECTION('',(0.,0.,-1.));
#17031=DIRECTION('',(-1.,0.,0.));
#17032=DIRECTION('',(0.,-1.,0.));
#17033=DIRECTION('',(0.,-1.,0.));
#17034=DIRECTION('',(0.,0.,-1.));
#17035=DIRECTION('',(0.,-1.,0.));
#17036=DIRECTION('',(-0.923879532511286,0.,0.382683432365092));
#17037=DIRECTION('',(0.382683432365092,0.,0.923879532511286));
#17038=DIRECTION('',(0.,-1.,0.));
#17039=DIRECTION('',(0.130526192220052,0.,-0.99144486137381));
#17040=DIRECTION('',(-0.99144486137381,0.,-0.130526192220052));
#17041=DIRECTION('',(0.,-1.,0.));
#17042=DIRECTION('',(0.,-1.,0.));
#17043=DIRECTION('',(0.,0.,-1.));
#17044=DIRECTION('',(0.,-1.,0.));
#17045=DIRECTION('',(-0.965925826289068,0.,0.258819045102521));
#17046=DIRECTION('',(0.258819045102521,0.,0.965925826289068));
#17047=DIRECTION('',(0.,-1.,0.));
#17048=DIRECTION('',(0.258819045102521,0.,-0.965925826289068));
#17049=DIRECTION('',(-0.965925826289068,0.,-0.258819045102521));
#17050=DIRECTION('',(0.,-1.,0.));
#17051=DIRECTION('',(0.,-1.,0.));
#17052=DIRECTION('',(0.,0.,-1.));
#17053=DIRECTION('',(0.,-1.,0.));
#17054=DIRECTION('',(-0.99144486137381,0.,0.130526192220051));
#17055=DIRECTION('',(0.130526192220051,0.,0.99144486137381));
#17056=DIRECTION('',(0.,-1.,0.));
#17057=DIRECTION('',(0.382683432365089,0.,-0.923879532511287));
#17058=DIRECTION('',(-0.923879532511287,0.,-0.382683432365089));
#17059=DIRECTION('',(0.,-1.,0.));
#17060=DIRECTION('',(0.,-1.,0.));
#17061=DIRECTION('',(0.,0.,-1.));
#17062=DIRECTION('',(0.,-1.,0.));
#17063=DIRECTION('',(-1.,0.,0.));
#17064=DIRECTION('',(0.,0.,1.));
#17065=DIRECTION('',(0.,-1.,0.));
#17066=DIRECTION('',(0.5,0.,-0.866025403784439));
#17067=DIRECTION('',(-0.866025403784439,0.,-0.5));
#17068=DIRECTION('',(0.,-1.,0.));
#17069=DIRECTION('',(0.,-1.,0.));
#17070=DIRECTION('',(0.,0.,-1.));
#17071=DIRECTION('',(0.,-1.,0.));
#17072=DIRECTION('',(-0.99144486137381,0.,-0.130526192220052));
#17073=DIRECTION('',(-0.130526192220052,0.,0.99144486137381));
#17074=DIRECTION('',(0.,-1.,0.));
#17075=DIRECTION('',(0.608761429008722,0.,-0.793353340291235));
#17076=DIRECTION('',(-0.793353340291235,0.,-0.608761429008722));
#17077=DIRECTION('',(0.,-1.,0.));
#17078=DIRECTION('',(0.,-1.,0.));
#17079=DIRECTION('',(0.,0.,-1.));
#17080=DIRECTION('',(0.,-1.,0.));
#17081=DIRECTION('',(-0.965925826289068,0.,-0.258819045102521));
#17082=DIRECTION('',(-0.258819045102521,0.,0.965925826289068));
#17083=DIRECTION('',(0.,-1.,0.));
#17084=DIRECTION('',(0.707106781186548,0.,-0.707106781186548));
#17085=DIRECTION('',(-0.707106781186548,0.,-0.707106781186548));
#17086=DIRECTION('',(0.,-1.,0.));
#17087=DIRECTION('',(0.,-1.,0.));
#17088=DIRECTION('',(0.,0.,-1.));
#17089=DIRECTION('',(0.,-1.,0.));
#17090=DIRECTION('',(-0.923879532511287,0.,-0.38268343236509));
#17091=DIRECTION('',(-0.38268343236509,0.,0.923879532511287));
#17092=DIRECTION('',(0.,-1.,0.));
#17093=DIRECTION('',(0.793353340291235,0.,-0.608761429008721));
#17094=DIRECTION('',(-0.608761429008721,0.,-0.793353340291235));
#17095=DIRECTION('',(0.,-1.,0.));
#17096=DIRECTION('',(0.,-1.,0.));
#17097=DIRECTION('',(0.,0.,-1.));
#17098=DIRECTION('',(0.,-1.,0.));
#17099=DIRECTION('',(-0.866025403784439,0.,-0.5));
#17100=DIRECTION('',(-0.5,0.,0.866025403784439));
#17101=DIRECTION('',(0.,-1.,0.));
#17102=DIRECTION('',(0.866025403784439,0.,-0.5));
#17103=DIRECTION('',(-0.5,0.,-0.866025403784439));
#17104=DIRECTION('',(0.,-1.,0.));
#17105=DIRECTION('',(0.,-1.,0.));
#17106=DIRECTION('',(0.,0.,-1.));
#17107=DIRECTION('',(0.,-1.,0.));
#17108=DIRECTION('',(-0.793353340291234,0.,-0.608761429008722));
#17109=DIRECTION('',(-0.608761429008722,0.,0.793353340291234));
#17110=DIRECTION('',(0.,-1.,0.));
#17111=DIRECTION('',(0.923879532511287,0.,-0.38268343236509));
#17112=DIRECTION('',(-0.38268343236509,0.,-0.923879532511287));
#17113=DIRECTION('',(0.,-1.,0.));
#17114=DIRECTION('',(0.,-1.,0.));
#17115=DIRECTION('',(0.,0.,-1.));
#17116=DIRECTION('',(0.,-1.,0.));
#17117=DIRECTION('',(-0.707106781186548,0.,-0.707106781186548));
#17118=DIRECTION('',(-0.707106781186548,0.,0.707106781186548));
#17119=DIRECTION('',(0.,-1.,0.));
#17120=DIRECTION('',(0.965925826289068,0.,-0.258819045102522));
#17121=DIRECTION('',(-0.258819045102522,0.,-0.965925826289068));
#17122=DIRECTION('',(0.,-1.,0.));
#17123=DIRECTION('',(0.,-1.,0.));
#17124=DIRECTION('',(0.,0.,-1.));
#17125=DIRECTION('',(0.,-1.,0.));
#17126=DIRECTION('',(-0.608761429008721,0.,-0.793353340291235));
#17127=DIRECTION('',(-0.793353340291235,0.,0.608761429008721));
#17128=DIRECTION('',(0.,-1.,0.));
#17129=DIRECTION('',(0.99144486137381,0.,-0.130526192220053));
#17130=DIRECTION('',(-0.130526192220053,0.,-0.99144486137381));
#17131=DIRECTION('',(0.,-1.,0.));
#17132=DIRECTION('',(0.,-1.,0.));
#17133=DIRECTION('',(0.,0.,-1.));
#17134=DIRECTION('',(0.,-1.,0.));
#17135=DIRECTION('',(-0.5,0.,-0.866025403784439));
#17136=DIRECTION('',(-0.866025403784439,0.,0.5));
#17137=DIRECTION('',(0.,-1.,0.));
#17138=DIRECTION('',(1.,0.,0.));
#17139=DIRECTION('',(0.,0.,-1.));
#17140=DIRECTION('',(0.,-1.,0.));
#17141=DIRECTION('',(0.,-1.,0.));
#17142=DIRECTION('',(0.,0.,-1.));
#17143=DIRECTION('',(0.,-1.,0.));
#17144=DIRECTION('',(-0.38268343236509,0.,-0.923879532511287));
#17145=DIRECTION('',(-0.923879532511287,0.,0.38268343236509));
#17146=DIRECTION('',(0.,-1.,0.));
#17147=DIRECTION('',(0.991444861373811,0.,0.130526192220051));
#17148=DIRECTION('',(0.130526192220051,0.,-0.991444861373811));
#17149=DIRECTION('',(0.,-1.,0.));
#17150=DIRECTION('',(0.,-1.,0.));
#17151=DIRECTION('',(0.,0.,-1.));
#17152=DIRECTION('',(0.,-1.,0.));
#17153=DIRECTION('',(-0.258819045102521,0.,-0.965925826289068));
#17154=DIRECTION('',(-0.965925826289068,0.,0.258819045102521));
#17155=DIRECTION('',(0.,-1.,0.));
#17156=DIRECTION('',(0.965925826289069,0.,0.258819045102519));
#17157=DIRECTION('',(0.258819045102519,0.,-0.965925826289069));
#17158=DIRECTION('',(0.,-1.,0.));
#17159=DIRECTION('',(0.,-1.,0.));
#17160=DIRECTION('',(0.,0.,-1.));
#17161=DIRECTION('',(0.,-1.,0.));
#17162=DIRECTION('',(-0.130526192220052,0.,-0.99144486137381));
#17163=DIRECTION('',(-0.99144486137381,0.,0.130526192220052));
#17164=DIRECTION('',(0.,-1.,0.));
#17165=DIRECTION('',(0.923879532511288,0.,0.382683432365088));
#17166=DIRECTION('',(0.382683432365088,0.,-0.923879532511288));
#17167=DIRECTION('',(0.,-1.,0.));
#17168=DIRECTION('',(0.,-1.,0.));
#17169=DIRECTION('',(0.,0.,-1.));
#17170=DIRECTION('',(0.,-1.,0.));
#17171=DIRECTION('',(0.,0.,-1.));
#17172=DIRECTION('',(-1.,0.,0.));
#17173=DIRECTION('',(0.,-1.,0.));
#17174=DIRECTION('',(0.86602540378444,0.,0.5));
#17175=DIRECTION('',(0.5,0.,-0.86602540378444));
#17176=DIRECTION('',(0.,-1.,0.));
#17177=DIRECTION('',(0.,-1.,0.));
#17178=DIRECTION('',(0.,0.,-1.));
#17179=DIRECTION('',(0.,-1.,0.));
#17180=DIRECTION('',(0.130526192220052,0.,-0.99144486137381));
#17181=DIRECTION('',(-0.99144486137381,0.,-0.130526192220052));
#17182=DIRECTION('',(0.,-1.,0.));
#17183=DIRECTION('',(0.793353340291236,0.,0.608761429008719));
#17184=DIRECTION('',(0.608761429008719,0.,-0.793353340291236));
#17185=DIRECTION('',(0.,-1.,0.));
#17186=DIRECTION('',(0.,-1.,0.));
#17187=DIRECTION('',(0.,0.,-1.));
#17188=DIRECTION('',(0.,-1.,0.));
#17189=DIRECTION('',(0.258819045102521,0.,-0.965925826289068));
#17190=DIRECTION('',(-0.965925826289068,0.,-0.258819045102521));
#17191=DIRECTION('',(0.,-1.,0.));
#17192=DIRECTION('',(0.707106781186549,0.,0.707106781186546));
#17193=DIRECTION('',(0.707106781186546,0.,-0.707106781186549));
#17194=DIRECTION('',(0.,-1.,0.));
#17195=DIRECTION('',(0.,-1.,0.));
#17196=DIRECTION('',(0.,0.,-1.));
#17197=DIRECTION('',(0.,-1.,0.));
#17198=DIRECTION('',(0.382683432365089,0.,-0.923879532511287));
#17199=DIRECTION('',(-0.923879532511287,0.,-0.382683432365089));
#17200=DIRECTION('',(0.,-1.,0.));
#17201=DIRECTION('',(0.608761429008721,0.,0.793353340291235));
#17202=DIRECTION('',(0.793353340291235,0.,-0.608761429008721));
#17203=DIRECTION('',(0.,-1.,0.));
#17204=DIRECTION('',(0.,-1.,0.));
#17205=DIRECTION('',(0.,0.,-1.));
#17206=DIRECTION('',(0.,-1.,0.));
#17207=DIRECTION('',(0.5,0.,-0.866025403784439));
#17208=DIRECTION('',(-0.866025403784439,0.,-0.5));
#17209=DIRECTION('',(0.,-1.,0.));
#17210=DIRECTION('',(0.5,0.,0.866025403784438));
#17211=DIRECTION('',(0.866025403784438,0.,-0.5));
#17212=DIRECTION('',(0.,-1.,0.));
#17213=DIRECTION('',(0.,-1.,0.));
#17214=DIRECTION('',(0.,0.,-1.));
#17215=DIRECTION('',(0.,-1.,0.));
#17216=DIRECTION('',(0.608761429008722,0.,-0.793353340291235));
#17217=DIRECTION('',(-0.793353340291235,0.,-0.608761429008722));
#17218=DIRECTION('',(0.,-1.,0.));
#17219=DIRECTION('',(0.382683432365092,0.,0.923879532511286));
#17220=DIRECTION('',(0.923879532511286,0.,-0.382683432365092));
#17221=DIRECTION('',(0.,-1.,0.));
#17222=DIRECTION('',(0.,-1.,0.));
#17223=DIRECTION('',(0.,0.,-1.));
#17224=DIRECTION('',(0.,-1.,0.));
#17225=DIRECTION('',(0.707106781186548,0.,-0.707106781186548));
#17226=DIRECTION('',(-0.707106781186548,0.,-0.707106781186548));
#17227=DIRECTION('',(0.,-1.,0.));
#17228=DIRECTION('',(0.258819045102523,0.,0.965925826289068));
#17229=DIRECTION('',(0.965925826289068,0.,-0.258819045102523));
#17230=DIRECTION('',(0.,-1.,0.));
#17231=DIRECTION('',(0.,-1.,0.));
#17232=DIRECTION('',(0.,0.,-1.));
#17233=DIRECTION('',(0.,-1.,0.));
#17234=DIRECTION('',(0.793353340291235,0.,-0.608761429008721));
#17235=DIRECTION('',(-0.608761429008721,0.,-0.793353340291235));
#17236=DIRECTION('',(0.,-1.,0.));
#17237=DIRECTION('',(0.130526192220053,0.,0.99144486137381));
#17238=DIRECTION('',(0.99144486137381,0.,-0.130526192220053));
#17239=DIRECTION('',(0.,-1.,0.));
#17240=DIRECTION('',(0.,-1.,0.));
#17241=DIRECTION('',(0.,0.,-1.));
#17242=DIRECTION('',(0.,-1.,0.));
#17243=DIRECTION('',(0.866025403784439,0.,-0.5));
#17244=DIRECTION('',(-0.5,0.,-0.866025403784439));
#17245=DIRECTION('',(0.,-1.,0.));
#17246=DIRECTION('',(0.,0.,1.));
#17247=DIRECTION('',(1.,0.,0.));
#17248=DIRECTION('',(0.,-1.,0.));
#17249=DIRECTION('',(0.,-1.,0.));
#17250=DIRECTION('',(0.,0.,-1.));
#17251=DIRECTION('',(0.,-1.,0.));
#17252=DIRECTION('',(0.923879532511287,0.,-0.38268343236509));
#17253=DIRECTION('',(-0.38268343236509,0.,-0.923879532511287));
#17254=DIRECTION('',(0.,-1.,0.));
#17255=DIRECTION('',(-0.130526192220051,0.,0.991444861373811));
#17256=DIRECTION('',(0.991444861373811,0.,0.130526192220051));
#17257=DIRECTION('',(0.,-1.,0.));
#17258=DIRECTION('',(0.,-1.,0.));
#17259=DIRECTION('',(0.,0.,-1.));
#17260=DIRECTION('',(0.,-1.,0.));
#17261=DIRECTION('',(0.965925826289068,0.,-0.258819045102522));
#17262=DIRECTION('',(-0.258819045102522,0.,-0.965925826289068));
#17263=DIRECTION('',(0.,-1.,0.));
#17264=DIRECTION('',(-0.258819045102519,0.,0.965925826289069));
#17265=DIRECTION('',(0.965925826289069,0.,0.258819045102519));
#17266=DIRECTION('',(0.,-1.,0.));
#17267=DIRECTION('',(0.,-1.,0.));
#17268=DIRECTION('',(0.,0.,-1.));
#17269=DIRECTION('',(0.,-1.,0.));
#17270=DIRECTION('',(0.99144486137381,0.,-0.130526192220053));
#17271=DIRECTION('',(-0.130526192220053,0.,-0.99144486137381));
#17272=DIRECTION('',(0.,-1.,0.));
#17273=DIRECTION('',(-0.382683432365088,0.,0.923879532511288));
#17274=DIRECTION('',(0.923879532511288,0.,0.382683432365088));
#17275=DIRECTION('',(0.,-1.,0.));
#17276=DIRECTION('',(0.,-1.,0.));
#17277=DIRECTION('',(0.,0.,-1.));
#17278=DIRECTION('',(0.,-1.,0.));
#17279=DIRECTION('',(1.,0.,0.));
#17280=DIRECTION('',(0.,0.,-1.));
#17281=DIRECTION('',(0.,-1.,0.));
#17282=DIRECTION('',(-0.5,0.,0.86602540378444));
#17283=DIRECTION('',(0.86602540378444,0.,0.5));
#17284=DIRECTION('',(0.,-1.,0.));
#17285=DIRECTION('',(0.,-1.,0.));
#17286=DIRECTION('',(0.,0.,-1.));
#17287=DIRECTION('',(0.,-1.,0.));
#17288=DIRECTION('',(0.991444861373811,0.,0.130526192220051));
#17289=DIRECTION('',(0.130526192220051,0.,-0.991444861373811));
#17290=DIRECTION('',(0.,-1.,0.));
#17291=DIRECTION('',(-0.608761429008719,0.,0.793353340291236));
#17292=DIRECTION('',(0.793353340291236,0.,0.608761429008719));
#17293=DIRECTION('',(0.,-1.,0.));
#17294=DIRECTION('',(0.,-1.,0.));
#17295=DIRECTION('',(0.,0.,-1.));
#17296=DIRECTION('',(0.,-1.,0.));
#17297=DIRECTION('',(0.965925826289069,0.,0.258819045102519));
#17298=DIRECTION('',(0.258819045102519,0.,-0.965925826289069));
#17299=DIRECTION('',(0.,-1.,0.));
#17300=DIRECTION('',(-0.707106781186548,0.,0.707106781186548));
#17301=DIRECTION('',(0.707106781186548,0.,0.707106781186548));
#17302=DIRECTION('',(0.,-1.,0.));
#17303=DIRECTION('',(0.,-1.,0.));
#17304=DIRECTION('',(0.,0.,-1.));
#17305=DIRECTION('',(0.,-1.,0.));
#17306=DIRECTION('',(0.923879532511288,0.,0.382683432365088));
#17307=DIRECTION('',(0.382683432365088,0.,-0.923879532511288));
#17308=DIRECTION('',(0.,-1.,0.));
#17309=DIRECTION('',(-0.793353340291234,0.,0.608761429008723));
#17310=DIRECTION('',(0.608761429008723,0.,0.793353340291234));
#17311=DIRECTION('',(0.,-1.,0.));
#17312=DIRECTION('',(0.,-1.,0.));
#17313=DIRECTION('',(0.,0.,-1.));
#17314=DIRECTION('',(0.,-1.,0.));
#17315=DIRECTION('',(0.86602540378444,0.,0.5));
#17316=DIRECTION('',(0.5,0.,-0.86602540378444));
#17317=DIRECTION('',(0.,-1.,0.));
#17318=DIRECTION('',(-0.866025403784438,0.,0.5));
#17319=DIRECTION('',(0.5,0.,0.866025403784438));
#17320=DIRECTION('',(0.,-1.,0.));
#17321=DIRECTION('',(0.,-1.,0.));
#17322=DIRECTION('',(0.,0.,-1.));
#17323=DIRECTION('',(0.,-1.,0.));
#17324=DIRECTION('',(0.793353340291236,0.,0.608761429008719));
#17325=DIRECTION('',(0.608761429008719,0.,-0.793353340291236));
#17326=DIRECTION('',(0.,-1.,0.));
#17327=DIRECTION('',(-0.923879532511286,0.,0.382683432365092));
#17328=DIRECTION('',(0.382683432365092,0.,0.923879532511286));
#17329=DIRECTION('',(0.,-1.,0.));
#17330=DIRECTION('',(0.,-1.,0.));
#17331=DIRECTION('',(0.,0.,-1.));
#17332=DIRECTION('',(0.,-1.,0.));
#17333=DIRECTION('',(0.707106781186549,0.,0.707106781186546));
#17334=DIRECTION('',(0.707106781186546,0.,-0.707106781186549));
#17335=DIRECTION('',(0.,-1.,0.));
#17336=DIRECTION('',(-0.965925826289068,0.,0.258819045102521));
#17337=DIRECTION('',(0.258819045102521,0.,0.965925826289068));
#17338=DIRECTION('',(0.,-1.,0.));
#17339=DIRECTION('',(0.,-1.,0.));
#17340=DIRECTION('',(0.,0.,-1.));
#17341=DIRECTION('',(0.,-1.,0.));
#17342=DIRECTION('',(0.608761429008721,0.,0.793353340291235));
#17343=DIRECTION('',(0.793353340291235,0.,-0.608761429008721));
#17344=DIRECTION('',(0.,-1.,0.));
#17345=DIRECTION('',(-0.99144486137381,0.,0.130526192220051));
#17346=DIRECTION('',(0.130526192220051,0.,0.99144486137381));
#17347=DIRECTION('',(0.,-1.,0.));
#17348=DIRECTION('',(0.,-1.,0.));
#17349=DIRECTION('',(0.,0.,-1.));
#17350=DIRECTION('',(0.,-1.,0.));
#17351=DIRECTION('',(0.5,0.,0.866025403784438));
#17352=DIRECTION('',(0.866025403784438,0.,-0.5));
#17353=DIRECTION('',(0.,-1.,0.));
#17354=DIRECTION('',(-1.,0.,0.));
#17355=DIRECTION('',(0.,0.,1.));
#17356=DIRECTION('',(0.,-1.,0.));
#17357=DIRECTION('',(0.,-1.,0.));
#17358=DIRECTION('',(0.,0.,-1.));
#17359=DIRECTION('',(0.,-1.,0.));
#17360=DIRECTION('',(0.382683432365092,0.,0.923879532511286));
#17361=DIRECTION('',(0.923879532511286,0.,-0.382683432365092));
#17362=DIRECTION('',(0.,-1.,0.));
#17363=DIRECTION('',(-0.99144486137381,0.,-0.130526192220052));
#17364=DIRECTION('',(-0.130526192220052,0.,0.99144486137381));
#17365=DIRECTION('',(0.,-1.,0.));
#17366=DIRECTION('',(0.,-1.,0.));
#17367=DIRECTION('',(0.,0.,-1.));
#17368=DIRECTION('',(0.,-1.,0.));
#17369=DIRECTION('',(0.258819045102523,0.,0.965925826289068));
#17370=DIRECTION('',(0.965925826289068,0.,-0.258819045102523));
#17371=DIRECTION('',(0.,-1.,0.));
#17372=DIRECTION('',(-0.965925826289068,0.,-0.258819045102521));
#17373=DIRECTION('',(-0.258819045102521,0.,0.965925826289068));
#17374=DIRECTION('',(0.,-1.,0.));
#17375=DIRECTION('',(0.,-1.,0.));
#17376=DIRECTION('',(0.,0.,-1.));
#17377=DIRECTION('',(0.,-1.,0.));
#17378=DIRECTION('',(0.130526192220053,0.,0.99144486137381));
#17379=DIRECTION('',(0.99144486137381,0.,-0.130526192220053));
#17380=DIRECTION('',(0.,-1.,0.));
#17381=DIRECTION('',(-0.923965399010245,0.,-0.382476066482387));
#17382=DIRECTION('',(-0.382476066482387,0.,0.923965399010245));
#17383=DIRECTION('',(0.,-1.,0.));
#17384=DIRECTION('',(0.,0.,1.));
#17385=DIRECTION('',(1.,0.,0.));
#17386=DIRECTION('',(0.,-1.,0.));
#17387=DIRECTION('',(-0.866025403784439,0.,-0.5));
#17388=DIRECTION('',(-0.5,0.,0.866025403784439));
#17389=DIRECTION('',(0.,-1.,0.));
#17390=DIRECTION('',(0.,-1.,0.));
#17391=DIRECTION('',(0.,0.,-1.));
#17392=DIRECTION('',(0.,-1.,0.));
#17393=DIRECTION('',(-0.130526192220051,0.,0.991444861373811));
#17394=DIRECTION('',(0.991444861373811,0.,0.130526192220051));
#17395=DIRECTION('',(0.,-1.,0.));
#17396=DIRECTION('',(-0.793353340291234,0.,-0.608761429008722));
#17397=DIRECTION('',(-0.608761429008722,0.,0.793353340291234));
#17398=DIRECTION('',(0.,-1.,0.));
#17399=DIRECTION('',(0.,-1.,0.));
#17400=DIRECTION('',(0.,0.,-1.));
#17401=DIRECTION('',(0.,-1.,0.));
#17402=DIRECTION('',(-0.258819045102519,0.,0.965925826289069));
#17403=DIRECTION('',(0.965925826289069,0.,0.258819045102519));
#17404=DIRECTION('',(0.,-1.,0.));
#17405=DIRECTION('',(-0.707106781186548,0.,-0.707106781186548));
#17406=DIRECTION('',(-0.707106781186548,0.,0.707106781186548));
#17407=DIRECTION('',(0.,-1.,0.));
#17408=DIRECTION('',(0.,-1.,0.));
#17409=DIRECTION('',(0.,0.,-1.));
#17410=DIRECTION('',(0.,-1.,0.));
#17411=DIRECTION('',(-0.382683432365088,0.,0.923879532511288));
#17412=DIRECTION('',(0.923879532511288,0.,0.382683432365088));
#17413=DIRECTION('',(0.,-1.,0.));
#17414=DIRECTION('',(-0.608761429008721,0.,-0.793353340291235));
#17415=DIRECTION('',(-0.793353340291235,0.,0.608761429008721));
#17416=DIRECTION('',(0.,-1.,0.));
#17417=DIRECTION('',(0.,-1.,0.));
#17418=DIRECTION('',(0.,0.,-1.));
#17419=DIRECTION('',(0.,-1.,0.));
#17420=DIRECTION('',(-0.5,0.,0.86602540378444));
#17421=DIRECTION('',(0.86602540378444,0.,0.5));
#17422=DIRECTION('',(0.,-1.,0.));
#17423=DIRECTION('',(-0.5,0.,-0.866025403784439));
#17424=DIRECTION('',(-0.866025403784439,0.,0.5));
#17425=DIRECTION('',(0.,1.,0.));
#17426=DIRECTION('',(0.,0.,1.));
#17427=DIRECTION('',(0.,1.,0.));
#17428=DIRECTION('',(0.,0.,1.));
#17429=DIRECTION('',(0.,1.,0.));
#17430=DIRECTION('',(0.,0.,1.));
#17431=DIRECTION('',(0.,-1.,0.));
#17432=DIRECTION('',(0.,0.,-1.));
#17433=DIRECTION('',(0.,-1.,0.));
#17434=DIRECTION('',(0.,0.,-1.));
#17435=DIRECTION('',(0.,-1.,0.));
#17436=DIRECTION('',(0.,0.,-1.));
#17437=DIRECTION('',(0.,1.,0.));
#17438=DIRECTION('',(0.,0.,1.));
#17439=DIRECTION('',(0.,-1.,0.));
#17440=DIRECTION('',(0.,0.,-1.));
#17441=DIRECTION('',(0.,1.,0.));
#17442=DIRECTION('',(0.,0.,1.));
#17443=DIRECTION('',(0.,1.,0.));
#17444=DIRECTION('',(0.,0.,1.));
#17445=DIRECTION('',(0.,1.,0.));
#17446=DIRECTION('',(0.,0.,1.));
#19109=CARTESIAN_POINT('',(0.,0.,0.));
#33563=CARTESIAN_POINT('',(0.,0.00159300366304774,0.));
#33564=CARTESIAN_POINT('',(0.,0.00159300366304774,0.));
#33565=CARTESIAN_POINT('',(0.,0.00159300366304774,-0.001));
#33566=CARTESIAN_POINT('',(0.,0.000812378913247946,0.));
#33567=CARTESIAN_POINT('',(0.,0.000812378913247946,-0.000625));
#33568=CARTESIAN_POINT('',(-0.0033118988125,0.0113437500020484,0.));
#33569=CARTESIAN_POINT('',(-0.0033118988125,0.0112500000020484,-0.00137183340534485));
#33570=CARTESIAN_POINT('',(-0.00234186610892243,0.0111562500020484,-0.00234186610892243));
#33571=CARTESIAN_POINT('',(-0.00137183340534485,0.0110625000020484,-0.0033118988125));
#33572=CARTESIAN_POINT('',(-2.02795313991402E-19,0.0109687500020484,-0.0033118988125));
#33573=CARTESIAN_POINT('',(0.00137183340534485,0.0108750000020484,-0.0033118988125));
#33574=CARTESIAN_POINT('',(0.00234186610892243,0.0107812500020484,-0.00234186610892243));
#33575=CARTESIAN_POINT('',(0.0033118988125,0.0106875000020484,-0.00137183340534485));
#33576=CARTESIAN_POINT('',(0.0033118988125,0.0105937500020484,-4.05590627982804E-19));
#33577=CARTESIAN_POINT('',(0.0033118988125,0.0105000000020484,0.00137183340534485));
#33578=CARTESIAN_POINT('',(0.00234186610892243,0.0104062500020484,0.00234186610892243));
#33579=CARTESIAN_POINT('',(0.00137183340534485,0.0103125000020484,0.0033118988125));
#33580=CARTESIAN_POINT('',(6.08385941974207E-19,0.0102187500020484,0.0033118988125));
#33581=CARTESIAN_POINT('',(-0.00137183340534485,0.0101250000020484,0.0033118988125));
#33582=CARTESIAN_POINT('',(-0.00234186610892243,0.0100312500020484,0.00234186610892243));
#33583=CARTESIAN_POINT('',(-0.0033118988125,0.00993750000204839,0.00137183340534485));
#33584=CARTESIAN_POINT('',(-0.0033118988125,0.00984375000204839,0.));
#33585=CARTESIAN_POINT('',(-0.0033118988125,0.00975000000204839,-0.00137183340534485));
#33586=CARTESIAN_POINT('',(-0.00234186610892243,0.00965625000204839,-0.00234186610892243));
#33587=CARTESIAN_POINT('',(-0.00137183340534485,0.00956250000204839,-0.0033118988125));
#33588=CARTESIAN_POINT('',(-2.02795313991402E-19,0.00946875000204839,-0.0033118988125));
#33589=CARTESIAN_POINT('',(0.00137183340534485,0.00937500000204839,-0.0033118988125));
#33590=CARTESIAN_POINT('',(0.00234186610892243,0.00928125000204839,-0.00234186610892243));
#33591=CARTESIAN_POINT('',(0.0033118988125,0.00918750000204839,-0.00137183340534485));
#33592=CARTESIAN_POINT('',(0.0033118988125,0.00909375000204839,-4.05590627982804E-19));
#33593=CARTESIAN_POINT('',(0.0033118988125,0.00900000000204839,0.00137183340534485));
#33594=CARTESIAN_POINT('',(0.00234186610892243,0.00890625000204839,0.00234186610892243));
#33595=CARTESIAN_POINT('',(0.00137183340534485,0.00881250000204839,0.0033118988125));
#33596=CARTESIAN_POINT('',(6.08385941974207E-19,0.00871875000204839,0.0033118988125));
#33597=CARTESIAN_POINT('',(-0.00137183340534485,0.00862500000204838,0.0033118988125));
#33598=CARTESIAN_POINT('',(-0.00234186610892243,0.00853125000204839,0.00234186610892243));
#33599=CARTESIAN_POINT('',(-0.0033118988125,0.00843750000204839,0.00137183340534485));
#33600=CARTESIAN_POINT('',(-0.0033118988125,0.00834375000204839,0.));
#33601=CARTESIAN_POINT('',(-0.0033118988125,0.00825000000204839,-0.00137183340534485));
#33602=CARTESIAN_POINT('',(-0.00234186610892243,0.00815625000204839,-0.00234186610892243));
#33603=CARTESIAN_POINT('',(-0.00137183340534485,0.00806250000204838,-0.0033118988125));
#33604=CARTESIAN_POINT('',(-2.02795313991402E-19,0.00796875000204839,-0.0033118988125));
#33605=CARTESIAN_POINT('',(0.00137183340534485,0.00787500000204839,-0.0033118988125));
#33606=CARTESIAN_POINT('',(0.00234186610892243,0.00778125000204839,-0.00234186610892243));
#33607=CARTESIAN_POINT('',(0.0033118988125,0.00768750000204838,-0.00137183340534485));
#33608=CARTESIAN_POINT('',(0.0033118988125,0.00759375000204839,-4.05590627982804E-19));
#33609=CARTESIAN_POINT('',(0.0033118988125,0.00750000000204839,0.00137183340534485));
#33610=CARTESIAN_POINT('',(0.00234186610892243,0.00740625000204839,0.00234186610892243));
#33611=CARTESIAN_POINT('',(0.00137183340534485,0.00731250000204839,0.0033118988125));
#33612=CARTESIAN_POINT('',(6.08385941974207E-19,0.00721875000204839,0.0033118988125));
#33613=CARTESIAN_POINT('',(-0.00137183340534485,0.00712500000204838,0.0033118988125));
#33614=CARTESIAN_POINT('',(-0.00234186610892243,0.00703125000204839,0.00234186610892243));
#33615=CARTESIAN_POINT('',(-0.0033118988125,0.00693750000204839,0.00137183340534485));
#33616=CARTESIAN_POINT('',(-0.0033118988125,0.00684375000204839,0.));
#33617=CARTESIAN_POINT('',(-0.0033118988125,0.00675000000204839,-0.00137183340534485));
#33618=CARTESIAN_POINT('',(-0.00234186610892243,0.00665625000204839,-0.00234186610892243));
#33619=CARTESIAN_POINT('',(-0.00137183340534485,0.00656250000204838,-0.0033118988125));
#33620=CARTESIAN_POINT('',(-2.02795313991402E-19,0.00646875000204839,-0.0033118988125));
#33621=CARTESIAN_POINT('',(0.00137183340534485,0.00637500000204839,-0.0033118988125));
#33622=CARTESIAN_POINT('',(0.00234186610892243,0.00628125000204839,-0.00234186610892243));
#33623=CARTESIAN_POINT('',(0.0033118988125,0.00618750000204839,-0.00137183340534485));
#33624=CARTESIAN_POINT('',(0.0033118988125,0.00609375000204839,-4.05590627982804E-19));
#33625=CARTESIAN_POINT('',(-0.0025,0.0108750000040968,0.));
#33626=CARTESIAN_POINT('',(-0.0025,0.0107812500040968,-0.00103553390593274));
#33627=CARTESIAN_POINT('',(-0.00176776695296637,0.0106875000040968,-0.00176776695296637));
#33628=CARTESIAN_POINT('',(-0.00103553390593274,0.0105937500040968,-0.0025));
#33629=CARTESIAN_POINT('',(-1.53080849893419E-19,0.0105000000040968,-0.0025));
#33630=CARTESIAN_POINT('',(0.00103553390593274,0.0104062500040968,-0.0025));
#33631=CARTESIAN_POINT('',(0.00176776695296637,0.0103125000040968,-0.00176776695296637));
#33632=CARTESIAN_POINT('',(0.0025,0.0102187500040968,-0.00103553390593274));
#33633=CARTESIAN_POINT('',(0.0025,0.0101250000040968,-3.06161699786838E-19));
#33634=CARTESIAN_POINT('',(0.0025,0.0100312500040968,0.00103553390593274));
#33635=CARTESIAN_POINT('',(0.00176776695296637,0.00993750000409678,0.00176776695296637));
#33636=CARTESIAN_POINT('',(0.00103553390593274,0.00984375000409678,0.0025));
#33637=CARTESIAN_POINT('',(4.59242549680257E-19,0.00975000000409678,0.0025));
#33638=CARTESIAN_POINT('',(-0.00103553390593274,0.00965625000409677,0.0025));
#33639=CARTESIAN_POINT('',(-0.00176776695296637,0.00956250000409678,0.00176776695296637));
#33640=CARTESIAN_POINT('',(-0.0025,0.00946875000409678,0.00103553390593274));
#33641=CARTESIAN_POINT('',(-0.0025,0.00937500000409678,0.));
#33642=CARTESIAN_POINT('',(-0.0025,0.00928125000409678,-0.00103553390593274));
#33643=CARTESIAN_POINT('',(-0.00176776695296637,0.00918750000409678,-0.00176776695296637));
#33644=CARTESIAN_POINT('',(-0.00103553390593274,0.00909375000409678,-0.0025));
#33645=CARTESIAN_POINT('',(-1.53080849893419E-19,0.00900000000409678,-0.0025));
#33646=CARTESIAN_POINT('',(0.00103553390593274,0.00890625000409678,-0.0025));
#33647=CARTESIAN_POINT('',(0.00176776695296637,0.00881250000409678,-0.00176776695296637));
#33648=CARTESIAN_POINT('',(0.0025,0.00871875000409679,-0.00103553390593274));
#33649=CARTESIAN_POINT('',(0.0025,0.00862500000409678,-3.06161699786838E-19));
#33650=CARTESIAN_POINT('',(0.0025,0.00853125000409678,0.00103553390593274));
#33651=CARTESIAN_POINT('',(0.00176776695296637,0.00843750000409678,0.00176776695296637));
#33652=CARTESIAN_POINT('',(0.00103553390593274,0.00834375000409678,0.0025));
#33653=CARTESIAN_POINT('',(4.59242549680257E-19,0.00825000000409678,0.0025));
#33654=CARTESIAN_POINT('',(-0.00103553390593274,0.00815625000409678,0.0025));
#33655=CARTESIAN_POINT('',(-0.00176776695296637,0.00806250000409678,0.00176776695296637));
#33656=CARTESIAN_POINT('',(-0.0025,0.00796875000409678,0.00103553390593274));
#33657=CARTESIAN_POINT('',(-0.0025,0.00787500000409678,0.));
#33658=CARTESIAN_POINT('',(-0.0025,0.00778125000409678,-0.00103553390593274));
#33659=CARTESIAN_POINT('',(-0.00176776695296637,0.00768750000409678,-0.00176776695296637));
#33660=CARTESIAN_POINT('',(-0.00103553390593274,0.00759375000409678,-0.0025));
#33661=CARTESIAN_POINT('',(-1.53080849893419E-19,0.00750000000409678,-0.0025));
#33662=CARTESIAN_POINT('',(0.00103553390593274,0.00740625000409678,-0.0025));
#33663=CARTESIAN_POINT('',(0.00176776695296637,0.00731250000409678,-0.00176776695296637));
#33664=CARTESIAN_POINT('',(0.0025,0.00721875000409678,-0.00103553390593274));
#33665=CARTESIAN_POINT('',(0.0025,0.00712500000409678,-3.06161699786838E-19));
#33666=CARTESIAN_POINT('',(0.0025,0.00703125000409678,0.00103553390593274));
#33667=CARTESIAN_POINT('',(0.00176776695296637,0.00693750000409678,0.00176776695296637));
#33668=CARTESIAN_POINT('',(0.00103553390593274,0.00684375000409678,0.0025));
#33669=CARTESIAN_POINT('',(4.59242549680257E-19,0.00675000000409678,0.0025));
#33670=CARTESIAN_POINT('',(-0.00103553390593274,0.00665625000409677,0.0025));
#33671=CARTESIAN_POINT('',(-0.00176776695296637,0.00656250000409678,0.00176776695296637));
#33672=CARTESIAN_POINT('',(-0.0025,0.00646875000409678,0.00103553390593274));
#33673=CARTESIAN_POINT('',(-0.0025,0.00637500000409678,0.));
#33674=CARTESIAN_POINT('',(-0.0025,0.00628125000409678,-0.00103553390593274));
#33675=CARTESIAN_POINT('',(-0.00176776695296637,0.00618750000409678,-0.00176776695296637));
#33676=CARTESIAN_POINT('',(-0.00103553390593274,0.00609375000409678,-0.0025));
#33677=CARTESIAN_POINT('',(-1.53080849893419E-19,0.00600000000409678,-0.0025));
#33678=CARTESIAN_POINT('',(0.00103553390593274,0.00590625000409678,-0.0025));
#33679=CARTESIAN_POINT('',(0.00176776695296637,0.00581250000409678,-0.00176776695296637));
#33680=CARTESIAN_POINT('',(0.0025,0.00571875000409678,-0.00103553390593274));
#33681=CARTESIAN_POINT('',(0.0025,0.00562500000409678,-3.06161699786838E-19));
#33682=CARTESIAN_POINT('',(4.52517978168079E-11,0.006,-0.0025));
#33683=CARTESIAN_POINT('',(0.000745353373849253,0.006,-0.00261687718084826));
#33684=CARTESIAN_POINT('',(0.0022915751006763,0.00599999999999974,-0.00215635246836324));
#33685=CARTESIAN_POINT('',(0.00305646177817112,0.006,-0.000747630389407334));
#33686=CARTESIAN_POINT('',(0.00314951904574251,0.006,-3.85704841822218E-19));
#33687=CARTESIAN_POINT('',(4.52517979936896E-11,0.006,-0.0025));
#33688=CARTESIAN_POINT('',(0.00314951904574251,0.006,-3.85704841822218E-19));
#33689=CARTESIAN_POINT('',(4.59242549680257E-19,0.00675000000409678,0.0025));
#33690=CARTESIAN_POINT('',(-0.00103553390593274,0.00665625000409677,0.0025));
#33691=CARTESIAN_POINT('',(-0.00176776695296637,0.00656250000409678,0.00176776695296637));
#33692=CARTESIAN_POINT('',(-0.0025,0.00646875000409678,0.00103553390593274));
#33693=CARTESIAN_POINT('',(-0.0025,0.00637500000409678,0.));
#33694=CARTESIAN_POINT('',(-0.0025,0.00628125000409678,-0.00103553390593274));
#33695=CARTESIAN_POINT('',(-0.00176776695296637,0.00618750000409678,-0.00176776695296637));
#33696=CARTESIAN_POINT('',(-0.00103553390593274,0.00609375000409678,-0.0025));
#33697=CARTESIAN_POINT('',(4.52517978168079E-11,0.006,-0.0025));
#33698=CARTESIAN_POINT('',(4.59242549680257E-19,0.00675000000409678,0.0025));
#33699=CARTESIAN_POINT('',(-1.53080849893419E-19,0.00750000000409678,-0.0025));
#33700=CARTESIAN_POINT('',(0.00103553390593274,0.00740625000409678,-0.0025));
#33701=CARTESIAN_POINT('',(0.00176776695296637,0.00731250000409678,-0.00176776695296637));
#33702=CARTESIAN_POINT('',(0.0025,0.00721875000409678,-0.00103553390593274));
#33703=CARTESIAN_POINT('',(0.0025,0.00712500000409678,-3.06161699786838E-19));
#33704=CARTESIAN_POINT('',(0.0025,0.00703125000409678,0.00103553390593274));
#33705=CARTESIAN_POINT('',(0.00176776695296637,0.00693750000409678,0.00176776695296637));
#33706=CARTESIAN_POINT('',(0.00103553390593274,0.00684375000409678,0.0025));
#33707=CARTESIAN_POINT('',(4.59242549680257E-19,0.00675000000409678,0.0025));
#33708=CARTESIAN_POINT('',(-1.53080849893419E-19,0.00750000000409678,-0.0025));
#33709=CARTESIAN_POINT('',(4.59242549680257E-19,0.00825000000409678,0.0025));
#33710=CARTESIAN_POINT('',(-0.00103553390593274,0.00815625000409678,0.0025));
#33711=CARTESIAN_POINT('',(-0.00176776695296637,0.00806250000409678,0.00176776695296637));
#33712=CARTESIAN_POINT('',(-0.0025,0.00796875000409678,0.00103553390593274));
#33713=CARTESIAN_POINT('',(-0.0025,0.00787500000409678,0.));
#33714=CARTESIAN_POINT('',(-0.0025,0.00778125000409678,-0.00103553390593274));
#33715=CARTESIAN_POINT('',(-0.00176776695296637,0.00768750000409678,-0.00176776695296637));
#33716=CARTESIAN_POINT('',(-0.00103553390593274,0.00759375000409678,-0.0025));
#33717=CARTESIAN_POINT('',(-1.53080849893419E-19,0.00750000000409678,-0.0025));
#33718=CARTESIAN_POINT('',(4.59242549680257E-19,0.00825000000409678,0.0025));
#33719=CARTESIAN_POINT('',(-1.53080849893419E-19,0.00900000000409678,-0.0025));
#33720=CARTESIAN_POINT('',(0.00103553390593274,0.00890625000409678,-0.0025));
#33721=CARTESIAN_POINT('',(0.00176776695296637,0.00881250000409678,-0.00176776695296637));
#33722=CARTESIAN_POINT('',(0.0025,0.00871875000409679,-0.00103553390593274));
#33723=CARTESIAN_POINT('',(0.0025,0.00862500000409678,-3.06161699786838E-19));
#33724=CARTESIAN_POINT('',(0.0025,0.00853125000409678,0.00103553390593274));
#33725=CARTESIAN_POINT('',(0.00176776695296637,0.00843750000409678,0.00176776695296637));
#33726=CARTESIAN_POINT('',(0.00103553390593274,0.00834375000409678,0.0025));
#33727=CARTESIAN_POINT('',(4.59242549680257E-19,0.00825000000409678,0.0025));
#33728=CARTESIAN_POINT('',(-1.53080849893419E-19,0.00900000000409678,-0.0025));
#33729=CARTESIAN_POINT('',(4.59242549680257E-19,0.00975000000409678,0.0025));
#33730=CARTESIAN_POINT('',(-0.00103553390593274,0.00965625000409677,0.0025));
#33731=CARTESIAN_POINT('',(-0.00176776695296637,0.00956250000409678,0.00176776695296637));
#33732=CARTESIAN_POINT('',(-0.0025,0.00946875000409678,0.00103553390593274));
#33733=CARTESIAN_POINT('',(-0.0025,0.00937500000409678,0.));
#33734=CARTESIAN_POINT('',(-0.0025,0.00928125000409678,-0.00103553390593274));
#33735=CARTESIAN_POINT('',(-0.00176776695296637,0.00918750000409678,-0.00176776695296637));
#33736=CARTESIAN_POINT('',(-0.00103553390593274,0.00909375000409678,-0.0025));
#33737=CARTESIAN_POINT('',(-1.53080849893419E-19,0.00900000000409678,-0.0025));
#33738=CARTESIAN_POINT('',(4.59242549680257E-19,0.00975000000409678,0.0025));
#33739=CARTESIAN_POINT('',(-1.53080849893419E-19,0.0105000000040968,-0.0025));
#33740=CARTESIAN_POINT('',(0.00103553390593274,0.0104062500040968,-0.0025));
#33741=CARTESIAN_POINT('',(0.00176776695296637,0.0103125000040968,-0.00176776695296637));
#33742=CARTESIAN_POINT('',(0.0025,0.0102187500040968,-0.00103553390593274));
#33743=CARTESIAN_POINT('',(0.0025,0.0101250000040968,-3.06161699786838E-19));
#33744=CARTESIAN_POINT('',(0.0025,0.0100312500040968,0.00103553390593274));
#33745=CARTESIAN_POINT('',(0.00176776695296637,0.00993750000409678,0.00176776695296637));
#33746=CARTESIAN_POINT('',(0.00103553390593274,0.00984375000409678,0.0025));
#33747=CARTESIAN_POINT('',(4.59242549680257E-19,0.00975000000409678,0.0025));
#33748=CARTESIAN_POINT('',(-1.53080849893419E-19,0.0105000000040968,-0.0025));
#33749=CARTESIAN_POINT('',(-0.0025,0.0108750000040968,0.));
#33750=CARTESIAN_POINT('',(-0.0025,0.0107812500040968,-0.00103553390593274));
#33751=CARTESIAN_POINT('',(-0.00176776695296637,0.0106875000040968,-0.00176776695296637));
#33752=CARTESIAN_POINT('',(-0.00103553390593274,0.0105937500040968,-0.0025));
#33753=CARTESIAN_POINT('',(-1.53080849893419E-19,0.0105000000040968,-0.0025));
#33754=CARTESIAN_POINT('',(-0.0025,0.0108750000040968,0.));
#33755=CARTESIAN_POINT('',(-0.00290594940625,0.0111093750030726,0.));
#33756=CARTESIAN_POINT('',(-0.0033118988125,0.0113437500020484,0.));
#33757=CARTESIAN_POINT('',(-0.0033118988125,0.0113437500020484,0.));
#33758=CARTESIAN_POINT('',(-0.0033118988125,0.0112500000020484,-0.00137183340534485));
#33759=CARTESIAN_POINT('',(-0.00234186610892243,0.0111562500020484,-0.00234186610892243));
#33760=CARTESIAN_POINT('',(-0.00137183340534485,0.0110625000020484,-0.0033118988125));
#33761=CARTESIAN_POINT('',(-2.02795313991402E-19,0.0109687500020484,-0.0033118988125));
#33762=CARTESIAN_POINT('',(0.00137183340534485,0.0108750000020484,-0.0033118988125));
#33763=CARTESIAN_POINT('',(0.00234186610892243,0.0107812500020484,-0.00234186610892243));
#33764=CARTESIAN_POINT('',(0.0033118988125,0.0106875000020484,-0.00137183340534485));
#33765=CARTESIAN_POINT('',(0.0033118988125,0.0105937500020484,-4.05590627982804E-19));
#33766=CARTESIAN_POINT('',(0.0033118988125,0.0105000000020484,0.00137183340534485));
#33767=CARTESIAN_POINT('',(0.00234186610892243,0.0104062500020484,0.00234186610892243));
#33768=CARTESIAN_POINT('',(0.00137183340534485,0.0103125000020484,0.0033118988125));
#33769=CARTESIAN_POINT('',(6.08385941974207E-19,0.0102187500020484,0.0033118988125));
#33770=CARTESIAN_POINT('',(-0.00137183340534485,0.0101250000020484,0.0033118988125));
#33771=CARTESIAN_POINT('',(-0.00234186610892243,0.0100312500020484,0.00234186610892243));
#33772=CARTESIAN_POINT('',(-0.0033118988125,0.00993750000204839,0.00137183340534485));
#33773=CARTESIAN_POINT('',(-0.0033118988125,0.00984375000204839,0.));
#33774=CARTESIAN_POINT('',(-0.0033118988125,0.00975000000204839,-0.00137183340534485));
#33775=CARTESIAN_POINT('',(-0.00234186610892243,0.00965625000204839,-0.00234186610892243));
#33776=CARTESIAN_POINT('',(-0.00137183340534485,0.00956250000204839,-0.0033118988125));
#33777=CARTESIAN_POINT('',(-2.02795313991402E-19,0.00946875000204839,-0.0033118988125));
#33778=CARTESIAN_POINT('',(0.00137183340534485,0.00937500000204839,-0.0033118988125));
#33779=CARTESIAN_POINT('',(0.00234186610892243,0.00928125000204839,-0.00234186610892243));
#33780=CARTESIAN_POINT('',(0.0033118988125,0.00918750000204839,-0.00137183340534485));
#33781=CARTESIAN_POINT('',(0.0033118988125,0.00909375000204839,-4.05590627982804E-19));
#33782=CARTESIAN_POINT('',(0.0033118988125,0.00900000000204839,0.00137183340534485));
#33783=CARTESIAN_POINT('',(0.00234186610892243,0.00890625000204839,0.00234186610892243));
#33784=CARTESIAN_POINT('',(0.00137183340534485,0.00881250000204839,0.0033118988125));
#33785=CARTESIAN_POINT('',(6.08385941974207E-19,0.00871875000204839,0.0033118988125));
#33786=CARTESIAN_POINT('',(-0.00137183340534485,0.00862500000204838,0.0033118988125));
#33787=CARTESIAN_POINT('',(-0.00234186610892243,0.00853125000204839,0.00234186610892243));
#33788=CARTESIAN_POINT('',(-0.0033118988125,0.00843750000204839,0.00137183340534485));
#33789=CARTESIAN_POINT('',(-0.0033118988125,0.00834375000204839,0.));
#33790=CARTESIAN_POINT('',(-0.0033118988125,0.00825000000204839,-0.00137183340534485));
#33791=CARTESIAN_POINT('',(-0.00234186610892243,0.00815625000204839,-0.00234186610892243));
#33792=CARTESIAN_POINT('',(-0.00137183340534485,0.00806250000204839,-0.0033118988125));
#33793=CARTESIAN_POINT('',(-2.02795313991402E-19,0.00796875000204839,-0.0033118988125));
#33794=CARTESIAN_POINT('',(0.00137183340534485,0.00787500000204839,-0.0033118988125));
#33795=CARTESIAN_POINT('',(0.00234186610892243,0.00778125000204839,-0.00234186610892243));
#33796=CARTESIAN_POINT('',(0.0033118988125,0.00768750000204838,-0.00137183340534485));
#33797=CARTESIAN_POINT('',(0.0033118988125,0.00759375000204839,-4.05590627982804E-19));
#33798=CARTESIAN_POINT('',(0.0033118988125,0.00750000000204839,0.00137183340534485));
#33799=CARTESIAN_POINT('',(0.00234186610892243,0.00740625000204839,0.00234186610892243));
#33800=CARTESIAN_POINT('',(0.00137183340534485,0.00731250000204839,0.0033118988125));
#33801=CARTESIAN_POINT('',(6.08385941974207E-19,0.00721875000204839,0.0033118988125));
#33802=CARTESIAN_POINT('',(-0.00137183340534485,0.00712500000204839,0.0033118988125));
#33803=CARTESIAN_POINT('',(-0.00234186610892243,0.00703125000204839,0.00234186610892243));
#33804=CARTESIAN_POINT('',(-0.0033118988125,0.00693750000204839,0.00137183340534485));
#33805=CARTESIAN_POINT('',(-0.0033118988125,0.00684375000204839,0.));
#33806=CARTESIAN_POINT('',(-0.0033118988125,0.00675000000204839,-0.00137183340534485));
#33807=CARTESIAN_POINT('',(-0.00234186610892243,0.00665625000204839,-0.00234186610892243));
#33808=CARTESIAN_POINT('',(-0.00137183340534485,0.00656250000204838,-0.0033118988125));
#33809=CARTESIAN_POINT('',(-2.02795313991402E-19,0.00646875000204839,-0.0033118988125));
#33810=CARTESIAN_POINT('',(0.00137183340534485,0.00637500000204839,-0.0033118988125));
#33811=CARTESIAN_POINT('',(0.00234186610892243,0.00628125000204839,-0.00234186610892243));
#33812=CARTESIAN_POINT('',(0.0033118988125,0.00618750000204839,-0.00137183340534485));
#33813=CARTESIAN_POINT('',(0.0033118988125,0.00609375000204839,-4.05590627982804E-19));
#33814=CARTESIAN_POINT('',(0.00331189864583333,0.00609375009827343,-4.05590607572024E-19));
#33815=CARTESIAN_POINT('',(0.00323070892912125,0.0060468750010242,-3.95647734902512E-19));
#33816=CARTESIAN_POINT('',(-0.0025,0.012,0.));
#33817=CARTESIAN_POINT('',(-0.0025,0.01190625,-0.00103553390593274));
#33818=CARTESIAN_POINT('',(-0.00176776695296637,0.0118125,-0.00176776695296637));
#33819=CARTESIAN_POINT('',(-0.00103553390593274,0.01171875,-0.0025));
#33820=CARTESIAN_POINT('',(-1.53080849893419E-19,0.011625,-0.0025));
#33821=CARTESIAN_POINT('',(0.00103553390593274,0.01153125,-0.0025));
#33822=CARTESIAN_POINT('',(0.00176776695296637,0.0114375,-0.00176776695296637));
#33823=CARTESIAN_POINT('',(0.0025,0.01134375,-0.00103553390593274));
#33824=CARTESIAN_POINT('',(0.0025,0.01125,-3.06161699786838E-19));
#33825=CARTESIAN_POINT('',(0.0025,0.01115625,0.00103553390593274));
#33826=CARTESIAN_POINT('',(0.00176776695296637,0.0110625,0.00176776695296637));
#33827=CARTESIAN_POINT('',(0.00103553390593274,0.01096875,0.0025));
#33828=CARTESIAN_POINT('',(4.59242549680257E-19,0.010875,0.0025));
#33829=CARTESIAN_POINT('',(-0.00103553390593274,0.01078125,0.0025));
#33830=CARTESIAN_POINT('',(-0.00176776695296637,0.0106875,0.00176776695296637));
#33831=CARTESIAN_POINT('',(-0.0025,0.01059375,0.00103553390593274));
#33832=CARTESIAN_POINT('',(-0.0025,0.0105,0.));
#33833=CARTESIAN_POINT('',(-0.0025,0.01040625,-0.00103553390593274));
#33834=CARTESIAN_POINT('',(-0.00176776695296637,0.0103125,-0.00176776695296637));
#33835=CARTESIAN_POINT('',(-0.00103553390593274,0.01021875,-0.0025));
#33836=CARTESIAN_POINT('',(-1.53080849893419E-19,0.010125,-0.0025));
#33837=CARTESIAN_POINT('',(0.00103553390593274,0.01003125,-0.0025));
#33838=CARTESIAN_POINT('',(0.00176776695296637,0.0099375,-0.00176776695296637));
#33839=CARTESIAN_POINT('',(0.0025,0.00984375,-0.00103553390593274));
#33840=CARTESIAN_POINT('',(0.0025,0.00975,-3.06161699786838E-19));
#33841=CARTESIAN_POINT('',(0.0025,0.00965624999999999,0.00103553390593274));
#33842=CARTESIAN_POINT('',(0.00176776695296637,0.0095625,0.00176776695296637));
#33843=CARTESIAN_POINT('',(0.00103553390593274,0.00946875,0.0025));
#33844=CARTESIAN_POINT('',(4.59242549680257E-19,0.009375,0.0025));
#33845=CARTESIAN_POINT('',(-0.00103553390593274,0.00928125,0.0025));
#33846=CARTESIAN_POINT('',(-0.00176776695296637,0.0091875,0.00176776695296637));
#33847=CARTESIAN_POINT('',(-0.0025,0.00909374999999999,0.00103553390593274));
#33848=CARTESIAN_POINT('',(-0.0025,0.009,0.));
#33849=CARTESIAN_POINT('',(-0.0025,0.00890625,-0.00103553390593274));
#33850=CARTESIAN_POINT('',(-0.00176776695296637,0.0088125,-0.00176776695296637));
#33851=CARTESIAN_POINT('',(-0.00103553390593274,0.00871875,-0.0025));
#33852=CARTESIAN_POINT('',(-1.53080849893419E-19,0.008625,-0.0025));
#33853=CARTESIAN_POINT('',(0.00103553390593274,0.00853125,-0.0025));
#33854=CARTESIAN_POINT('',(0.00176776695296637,0.0084375,-0.00176776695296637));
#33855=CARTESIAN_POINT('',(0.0025,0.00834375,-0.00103553390593274));
#33856=CARTESIAN_POINT('',(0.0025,0.00825,-3.06161699786838E-19));
#33857=CARTESIAN_POINT('',(0.0025,0.00815625,0.00103553390593274));
#33858=CARTESIAN_POINT('',(0.00176776695296637,0.0080625,0.00176776695296637));
#33859=CARTESIAN_POINT('',(0.00103553390593274,0.00796875,0.0025));
#33860=CARTESIAN_POINT('',(4.59242549680257E-19,0.007875,0.0025));
#33861=CARTESIAN_POINT('',(-0.00103553390593274,0.00778125,0.0025));
#33862=CARTESIAN_POINT('',(-0.00176776695296637,0.0076875,0.00176776695296637));
#33863=CARTESIAN_POINT('',(-0.0025,0.00759374999999999,0.00103553390593274));
#33864=CARTESIAN_POINT('',(-0.0025,0.0075,0.));
#33865=CARTESIAN_POINT('',(-0.0025,0.00740625,-0.00103553390593274));
#33866=CARTESIAN_POINT('',(-0.00176776695296637,0.0073125,-0.00176776695296637));
#33867=CARTESIAN_POINT('',(-0.00103553390593274,0.00721875,-0.0025));
#33868=CARTESIAN_POINT('',(-1.53080849893419E-19,0.007125,-0.0025));
#33869=CARTESIAN_POINT('',(0.00103553390593274,0.00703124999999999,-0.0025));
#33870=CARTESIAN_POINT('',(0.00176776695296637,0.0069375,-0.00176776695296637));
#33871=CARTESIAN_POINT('',(0.0025,0.00684375,-0.00103553390593274));
#33872=CARTESIAN_POINT('',(0.0025,0.00675,-3.06161699786838E-19));
#33873=CARTESIAN_POINT('',(-0.0033118988125,0.0115312500020484,0.));
#33874=CARTESIAN_POINT('',(-0.0033118988125,0.0114375000020484,-0.00137183340534485));
#33875=CARTESIAN_POINT('',(-0.00234186610892243,0.0113437500020484,-0.00234186610892243));
#33876=CARTESIAN_POINT('',(-0.00137183340534485,0.0112500000020484,-0.0033118988125));
#33877=CARTESIAN_POINT('',(-2.02795313991402E-19,0.0111562500020484,-0.0033118988125));
#33878=CARTESIAN_POINT('',(0.00137183340534485,0.0110625000020484,-0.0033118988125));
#33879=CARTESIAN_POINT('',(0.00234186610892243,0.0109687500020484,-0.00234186610892243));
#33880=CARTESIAN_POINT('',(0.0033118988125,0.0108750000020484,-0.00137183340534485));
#33881=CARTESIAN_POINT('',(0.0033118988125,0.0107812500020484,-4.05590627982804E-19));
#33882=CARTESIAN_POINT('',(0.0033118988125,0.0106875000020484,0.00137183340534485));
#33883=CARTESIAN_POINT('',(0.00234186610892243,0.0105937500020484,0.00234186610892243));
#33884=CARTESIAN_POINT('',(0.00137183340534485,0.0105000000020484,0.0033118988125));
#33885=CARTESIAN_POINT('',(6.08385941974207E-19,0.0104062500020484,0.0033118988125));
#33886=CARTESIAN_POINT('',(-0.00137183340534485,0.0103125000020484,0.0033118988125));
#33887=CARTESIAN_POINT('',(-0.00234186610892243,0.0102187500020484,0.00234186610892243));
#33888=CARTESIAN_POINT('',(-0.0033118988125,0.0101250000020484,0.00137183340534485));
#33889=CARTESIAN_POINT('',(-0.0033118988125,0.0100312500020484,0.));
#33890=CARTESIAN_POINT('',(-0.0033118988125,0.00993750000204839,-0.00137183340534485));
#33891=CARTESIAN_POINT('',(-0.00234186610892243,0.00984375000204839,-0.00234186610892243));
#33892=CARTESIAN_POINT('',(-0.00137183340534485,0.00975000000204839,-0.0033118988125));
#33893=CARTESIAN_POINT('',(-2.02795313991402E-19,0.00965625000204839,-0.0033118988125));
#33894=CARTESIAN_POINT('',(0.00137183340534485,0.00956250000204839,-0.0033118988125));
#33895=CARTESIAN_POINT('',(0.00234186610892243,0.00946875000204839,-0.00234186610892243));
#33896=CARTESIAN_POINT('',(0.0033118988125,0.00937500000204839,-0.00137183340534485));
#33897=CARTESIAN_POINT('',(0.0033118988125,0.00928125000204839,-4.05590627982804E-19));
#33898=CARTESIAN_POINT('',(0.0033118988125,0.00918750000204839,0.00137183340534485));
#33899=CARTESIAN_POINT('',(0.00234186610892243,0.00909375000204839,0.00234186610892243));
#33900=CARTESIAN_POINT('',(0.00137183340534485,0.00900000000204839,0.0033118988125));
#33901=CARTESIAN_POINT('',(6.08385941974207E-19,0.00890625000204839,0.0033118988125));
#33902=CARTESIAN_POINT('',(-0.00137183340534485,0.00881250000204839,0.0033118988125));
#33903=CARTESIAN_POINT('',(-0.00234186610892243,0.00871875000204839,0.00234186610892243));
#33904=CARTESIAN_POINT('',(-0.0033118988125,0.00862500000204838,0.00137183340534485));
#33905=CARTESIAN_POINT('',(-0.0033118988125,0.00853125000204839,0.));
#33906=CARTESIAN_POINT('',(-0.0033118988125,0.00843750000204839,-0.00137183340534485));
#33907=CARTESIAN_POINT('',(-0.00234186610892243,0.00834375000204839,-0.00234186610892243));
#33908=CARTESIAN_POINT('',(-0.00137183340534485,0.00825000000204839,-0.0033118988125));
#33909=CARTESIAN_POINT('',(-2.02795313991402E-19,0.00815625000204839,-0.0033118988125));
#33910=CARTESIAN_POINT('',(0.00137183340534485,0.00806250000204838,-0.0033118988125));
#33911=CARTESIAN_POINT('',(0.00234186610892243,0.00796875000204839,-0.00234186610892243));
#33912=CARTESIAN_POINT('',(0.0033118988125,0.00787500000204839,-0.00137183340534485));
#33913=CARTESIAN_POINT('',(0.0033118988125,0.00778125000204839,-4.05590627982804E-19));
#33914=CARTESIAN_POINT('',(0.0033118988125,0.00768750000204838,0.00137183340534485));
#33915=CARTESIAN_POINT('',(0.00234186610892243,0.00759375000204839,0.00234186610892243));
#33916=CARTESIAN_POINT('',(0.00137183340534485,0.00750000000204839,0.0033118988125));
#33917=CARTESIAN_POINT('',(6.08385941974207E-19,0.00740625000204839,0.0033118988125));
#33918=CARTESIAN_POINT('',(-0.00137183340534485,0.00731250000204839,0.0033118988125));
#33919=CARTESIAN_POINT('',(-0.00234186610892243,0.00721875000204839,0.00234186610892243));
#33920=CARTESIAN_POINT('',(-0.0033118988125,0.00712500000204838,0.00137183340534485));
#33921=CARTESIAN_POINT('',(-0.0033118988125,0.00703125000204839,0.));
#33922=CARTESIAN_POINT('',(-0.0033118988125,0.00693750000204839,-0.00137183340534485));
#33923=CARTESIAN_POINT('',(-0.00234186610892243,0.00684375000204839,-0.00234186610892243));
#33924=CARTESIAN_POINT('',(-0.00137183340534485,0.00675000000204839,-0.0033118988125));
#33925=CARTESIAN_POINT('',(-2.02795313991402E-19,0.00665625000204839,-0.0033118988125));
#33926=CARTESIAN_POINT('',(0.00137183340534485,0.00656250000204838,-0.0033118988125));
#33927=CARTESIAN_POINT('',(0.00234186610892243,0.00646875000204839,-0.00234186610892243));
#33928=CARTESIAN_POINT('',(0.0033118988125,0.00637500000204839,-0.00137183340534485));
#33929=CARTESIAN_POINT('',(0.0033118988125,0.00628125000204839,-4.05590627982804E-19));
#33930=CARTESIAN_POINT('',(-0.00290594940625,0.0117656250010242,0.));
#33931=CARTESIAN_POINT('',(-0.0025,0.012,0.));
#33932=CARTESIAN_POINT('',(-0.0033118988125,0.0115312500020484,0.));
#33933=CARTESIAN_POINT('',(-0.0025,0.012,0.));
#33934=CARTESIAN_POINT('',(-0.0025,0.01190625,-0.00103553390593274));
#33935=CARTESIAN_POINT('',(-0.00176776695296637,0.0118125,-0.00176776695296637));
#33936=CARTESIAN_POINT('',(-0.00103553390593274,0.01171875,-0.0025));
#33937=CARTESIAN_POINT('',(-1.53080849893419E-19,0.011625,-0.0025));
#33938=CARTESIAN_POINT('',(-1.53080849893419E-19,0.011625,-0.0025));
#33939=CARTESIAN_POINT('',(-1.53080849893419E-19,0.011625,-0.0025));
#33940=CARTESIAN_POINT('',(0.00103553390593274,0.01153125,-0.0025));
#33941=CARTESIAN_POINT('',(0.00176776695296637,0.0114375,-0.00176776695296637));
#33942=CARTESIAN_POINT('',(0.0025,0.01134375,-0.00103553390593274));
#33943=CARTESIAN_POINT('',(0.0025,0.01125,-3.06161699786838E-19));
#33944=CARTESIAN_POINT('',(0.0025,0.01115625,0.00103553390593274));
#33945=CARTESIAN_POINT('',(0.00176776695296637,0.0110625,0.00176776695296637));
#33946=CARTESIAN_POINT('',(0.00103553390593274,0.01096875,0.0025));
#33947=CARTESIAN_POINT('',(4.59242549680257E-19,0.010875,0.0025));
#33948=CARTESIAN_POINT('',(4.59242549680257E-19,0.010875,0.0025));
#33949=CARTESIAN_POINT('',(4.59242549680257E-19,0.010875,0.0025));
#33950=CARTESIAN_POINT('',(-0.00103553390593274,0.01078125,0.0025));
#33951=CARTESIAN_POINT('',(-0.00176776695296637,0.0106875,0.00176776695296637));
#33952=CARTESIAN_POINT('',(-0.0025,0.01059375,0.00103553390593274));
#33953=CARTESIAN_POINT('',(-0.0025,0.0105,0.));
#33954=CARTESIAN_POINT('',(-0.0025,0.01040625,-0.00103553390593274));
#33955=CARTESIAN_POINT('',(-0.00176776695296637,0.0103125,-0.00176776695296637));
#33956=CARTESIAN_POINT('',(-0.00103553390593274,0.01021875,-0.0025));
#33957=CARTESIAN_POINT('',(-1.53080849893419E-19,0.010125,-0.0025));
#33958=CARTESIAN_POINT('',(-1.53080849893419E-19,0.010125,-0.0025));
#33959=CARTESIAN_POINT('',(-1.53080849893419E-19,0.010125,-0.0025));
#33960=CARTESIAN_POINT('',(0.00103553390593274,0.01003125,-0.0025));
#33961=CARTESIAN_POINT('',(0.00176776695296637,0.0099375,-0.00176776695296637));
#33962=CARTESIAN_POINT('',(0.0025,0.00984375,-0.00103553390593274));
#33963=CARTESIAN_POINT('',(0.0025,0.00975,-3.06161699786838E-19));
#33964=CARTESIAN_POINT('',(0.0025,0.00965624999999999,0.00103553390593274));
#33965=CARTESIAN_POINT('',(0.00176776695296637,0.0095625,0.00176776695296637));
#33966=CARTESIAN_POINT('',(0.00103553390593274,0.00946875,0.0025));
#33967=CARTESIAN_POINT('',(4.59242549680257E-19,0.009375,0.0025));
#33968=CARTESIAN_POINT('',(4.59242549680257E-19,0.009375,0.0025));
#33969=CARTESIAN_POINT('',(4.59242549680257E-19,0.009375,0.0025));
#33970=CARTESIAN_POINT('',(-0.00103553390593274,0.00928125,0.0025));
#33971=CARTESIAN_POINT('',(-0.00176776695296637,0.0091875,0.00176776695296637));
#33972=CARTESIAN_POINT('',(-0.0025,0.00909374999999999,0.00103553390593274));
#33973=CARTESIAN_POINT('',(-0.0025,0.009,0.));
#33974=CARTESIAN_POINT('',(-0.0025,0.00890625,-0.00103553390593274));
#33975=CARTESIAN_POINT('',(-0.00176776695296637,0.0088125,-0.00176776695296637));
#33976=CARTESIAN_POINT('',(-0.00103553390593274,0.00871875,-0.0025));
#33977=CARTESIAN_POINT('',(-1.53080849893419E-19,0.008625,-0.0025));
#33978=CARTESIAN_POINT('',(-1.53080849893419E-19,0.008625,-0.0025));
#33979=CARTESIAN_POINT('',(-1.53080849893419E-19,0.008625,-0.0025));
#33980=CARTESIAN_POINT('',(0.00103553390593274,0.00853125,-0.0025));
#33981=CARTESIAN_POINT('',(0.00176776695296637,0.0084375,-0.00176776695296637));
#33982=CARTESIAN_POINT('',(0.0025,0.00834375,-0.00103553390593274));
#33983=CARTESIAN_POINT('',(0.0025,0.00825,-3.06161699786838E-19));
#33984=CARTESIAN_POINT('',(0.0025,0.00815625,0.00103553390593274));
#33985=CARTESIAN_POINT('',(0.00176776695296637,0.0080625,0.00176776695296637));
#33986=CARTESIAN_POINT('',(0.00103553390593274,0.00796875,0.0025));
#33987=CARTESIAN_POINT('',(4.59242549680257E-19,0.007875,0.0025));
#33988=CARTESIAN_POINT('',(4.59242549680257E-19,0.007875,0.0025));
#33989=CARTESIAN_POINT('',(4.59242549680257E-19,0.007875,0.0025));
#33990=CARTESIAN_POINT('',(-0.00103553390593274,0.00778125,0.0025));
#33991=CARTESIAN_POINT('',(-0.00176776695296637,0.0076875,0.00176776695296637));
#33992=CARTESIAN_POINT('',(-0.0025,0.00759374999999999,0.00103553390593274));
#33993=CARTESIAN_POINT('',(-0.0025,0.0075,0.));
#33994=CARTESIAN_POINT('',(-0.0025,0.00740625,-0.00103553390593274));
#33995=CARTESIAN_POINT('',(-0.00176776695296637,0.0073125,-0.00176776695296637));
#33996=CARTESIAN_POINT('',(-0.00103553390593274,0.00721875,-0.0025));
#33997=CARTESIAN_POINT('',(-1.53080849893419E-19,0.007125,-0.0025));
#33998=CARTESIAN_POINT('',(-1.53080849893419E-19,0.007125,-0.0025));
#33999=CARTESIAN_POINT('',(-1.53080849893419E-19,0.007125,-0.0025));
#34000=CARTESIAN_POINT('',(0.00103553390593274,0.00703125,-0.0025));
#34001=CARTESIAN_POINT('',(0.00176776695296637,0.0069375,-0.00176776695296637));
#34002=CARTESIAN_POINT('',(0.0025,0.00684375,-0.00103553390593274));
#34003=CARTESIAN_POINT('',(0.0025,0.00675,-3.06161699786838E-19));
#34004=CARTESIAN_POINT('',(0.0025,0.00675,-3.06161699786838E-19));
#34005=CARTESIAN_POINT('',(0.00290594940625,0.00651562500102419,-3.55876163884822E-19));
#34006=CARTESIAN_POINT('',(0.00331189864583333,0.00628124990582335,-4.05590607572024E-19));
#34007=CARTESIAN_POINT('',(-0.0033118988125,0.0115312500020484,0.));
#34008=CARTESIAN_POINT('',(-0.0033118988125,0.0114375000020484,-0.00137183340534485));
#34009=CARTESIAN_POINT('',(-0.00234186610892243,0.0113437500020484,-0.00234186610892243));
#34010=CARTESIAN_POINT('',(-0.00137183340534485,0.0112500000020484,-0.0033118988125));
#34011=CARTESIAN_POINT('',(-2.02795313991402E-19,0.0111562500020484,-0.0033118988125));
#34012=CARTESIAN_POINT('',(0.00137183340534485,0.0110625000020484,-0.0033118988125));
#34013=CARTESIAN_POINT('',(0.00234186610892243,0.0109687500020484,-0.00234186610892243));
#34014=CARTESIAN_POINT('',(0.0033118988125,0.0108750000020484,-0.00137183340534485));
#34015=CARTESIAN_POINT('',(0.0033118988125,0.0107812500020484,-4.05590627982804E-19));
#34016=CARTESIAN_POINT('',(0.0033118988125,0.0106875000020484,0.00137183340534485));
#34017=CARTESIAN_POINT('',(0.00234186610892243,0.0105937500020484,0.00234186610892243));
#34018=CARTESIAN_POINT('',(0.00137183340534485,0.0105000000020484,0.0033118988125));
#34019=CARTESIAN_POINT('',(6.08385941974207E-19,0.0104062500020484,0.0033118988125));
#34020=CARTESIAN_POINT('',(-0.00137183340534485,0.0103125000020484,0.0033118988125));
#34021=CARTESIAN_POINT('',(-0.00234186610892243,0.0102187500020484,0.00234186610892243));
#34022=CARTESIAN_POINT('',(-0.0033118988125,0.0101250000020484,0.00137183340534485));
#34023=CARTESIAN_POINT('',(-0.0033118988125,0.0100312500020484,0.));
#34024=CARTESIAN_POINT('',(-0.0033118988125,0.00993750000204839,-0.00137183340534485));
#34025=CARTESIAN_POINT('',(-0.00234186610892243,0.00984375000204839,-0.00234186610892243));
#34026=CARTESIAN_POINT('',(-0.00137183340534485,0.00975000000204839,-0.0033118988125));
#34027=CARTESIAN_POINT('',(-2.02795313991402E-19,0.00965625000204839,-0.0033118988125));
#34028=CARTESIAN_POINT('',(0.00137183340534485,0.00956250000204839,-0.0033118988125));
#34029=CARTESIAN_POINT('',(0.00234186610892243,0.00946875000204839,-0.00234186610892243));
#34030=CARTESIAN_POINT('',(0.0033118988125,0.00937500000204839,-0.00137183340534485));
#34031=CARTESIAN_POINT('',(0.0033118988125,0.00928125000204839,-4.05590627982804E-19));
#34032=CARTESIAN_POINT('',(0.0033118988125,0.00918750000204839,0.00137183340534485));
#34033=CARTESIAN_POINT('',(0.00234186610892243,0.00909375000204839,0.00234186610892243));
#34034=CARTESIAN_POINT('',(0.00137183340534485,0.00900000000204839,0.0033118988125));
#34035=CARTESIAN_POINT('',(6.08385941974207E-19,0.00890625000204839,0.0033118988125));
#34036=CARTESIAN_POINT('',(-0.00137183340534485,0.00881250000204839,0.0033118988125));
#34037=CARTESIAN_POINT('',(-0.00234186610892243,0.00871875000204839,0.00234186610892243));
#34038=CARTESIAN_POINT('',(-0.0033118988125,0.00862500000204838,0.00137183340534485));
#34039=CARTESIAN_POINT('',(-0.0033118988125,0.00853125000204839,0.));
#34040=CARTESIAN_POINT('',(-0.0033118988125,0.00843750000204839,-0.00137183340534485));
#34041=CARTESIAN_POINT('',(-0.00234186610892243,0.00834375000204839,-0.00234186610892243));
#34042=CARTESIAN_POINT('',(-0.00137183340534485,0.00825000000204839,-0.0033118988125));
#34043=CARTESIAN_POINT('',(-2.02795313991402E-19,0.00815625000204839,-0.0033118988125));
#34044=CARTESIAN_POINT('',(0.00137183340534485,0.00806250000204839,-0.0033118988125));
#34045=CARTESIAN_POINT('',(0.00234186610892243,0.00796875000204839,-0.00234186610892243));
#34046=CARTESIAN_POINT('',(0.0033118988125,0.00787500000204839,-0.00137183340534485));
#34047=CARTESIAN_POINT('',(0.0033118988125,0.00778125000204839,-4.05590627982804E-19));
#34048=CARTESIAN_POINT('',(0.0033118988125,0.00768750000204838,0.00137183340534485));
#34049=CARTESIAN_POINT('',(0.00234186610892243,0.00759375000204839,0.00234186610892243));
#34050=CARTESIAN_POINT('',(0.00137183340534485,0.00750000000204839,0.0033118988125));
#34051=CARTESIAN_POINT('',(6.08385941974207E-19,0.00740625000204839,0.0033118988125));
#34052=CARTESIAN_POINT('',(-0.00137183340534485,0.00731250000204839,0.0033118988125));
#34053=CARTESIAN_POINT('',(-0.00234186610892243,0.00721875000204839,0.00234186610892243));
#34054=CARTESIAN_POINT('',(-0.0033118988125,0.00712500000204839,0.00137183340534485));
#34055=CARTESIAN_POINT('',(-0.0033118988125,0.00703125000204839,0.));
#34056=CARTESIAN_POINT('',(-0.0033118988125,0.00693750000204839,-0.00137183340534485));
#34057=CARTESIAN_POINT('',(-0.00234186610892243,0.00684375000204839,-0.00234186610892243));
#34058=CARTESIAN_POINT('',(-0.00137183340534485,0.00675000000204839,-0.0033118988125));
#34059=CARTESIAN_POINT('',(-2.02795313991402E-19,0.00665625000204839,-0.0033118988125));
#34060=CARTESIAN_POINT('',(0.00137183340534485,0.00656250000204838,-0.0033118988125));
#34061=CARTESIAN_POINT('',(0.00234186610892243,0.00646875000204839,-0.00234186610892243));
#34062=CARTESIAN_POINT('',(0.0033118988125,0.00637500000204839,-0.00137183340534485));
#34063=CARTESIAN_POINT('',(0.0033118988125,0.00628125000204839,-4.05590627982804E-19));
#34064=CARTESIAN_POINT('',(3.25260651745651E-18,0.0104430389370738,6.50521303491303E-18));
#34065=CARTESIAN_POINT('',(-0.0033118988125,0.0114375000020484,0.));
#34066=CARTESIAN_POINT('',(0.0033118988125,0.00618750000204839,-4.05590627982804E-19));
#34067=CARTESIAN_POINT('',(-0.0033118988125,0.0114375000020484,0.));
#34068=CARTESIAN_POINT('',(2.35858394177587E-50,0.006,1.92592994438723E-34));
#34069=CARTESIAN_POINT('',(0.0025,0.006,-3.38118020664279E-19));
#34070=CARTESIAN_POINT('',(0.0025,0.00614062500204839,-3.06161699786838E-19));
#34071=CARTESIAN_POINT('',(-0.0033118988125,0.0114375000020484,0.));
#34072=CARTESIAN_POINT('',(-0.0025,0.0114375000020484,0.));
#34073=CARTESIAN_POINT('',(0.,0.012,0.));
#34074=CARTESIAN_POINT('',(0.,0.012,0.));
#34075=CARTESIAN_POINT('',(0.,0.012,0.));
#34076=CARTESIAN_POINT('',(0.,0.012,0.002));
#34077=CARTESIAN_POINT('',(0.,0.,0.));
#34078=CARTESIAN_POINT('',(0.005,0.,0.));
#34079=CARTESIAN_POINT('',(0.00449037034920393,0.,0.000294234816074125));
#34080=CARTESIAN_POINT('',(0.005,2.89120579329468E-19,0.));
#34081=CARTESIAN_POINT('',(0.,0.,0.));
#34082=CARTESIAN_POINT('',(0.00449035995854428,0.,0.000294393346905451));
#34083=CARTESIAN_POINT('',(0.00495722430686905,0.,0.000652630961100258));
#34084=CARTESIAN_POINT('',(0.00495722430686905,2.89120579329468E-19,0.000652630961100258));
#34085=CARTESIAN_POINT('',(0.00495722430686905,0.,0.000652630961100258));
#34086=CARTESIAN_POINT('',(0.00441354925822283,0.,0.000877828539773374));
#34087=CARTESIAN_POINT('',(0.,0.,0.));
#34088=CARTESIAN_POINT('',(0.00441351826403096,0.,0.000877984358098221));
#34089=CARTESIAN_POINT('',(0.00482962913144534,0.,0.0012940952255126));
#34090=CARTESIAN_POINT('',(0.00482962913144534,0.,0.0012940952255126));
#34091=CARTESIAN_POINT('',(0.00482962913144534,0.,0.0012940952255126));
#34092=CARTESIAN_POINT('',(0.00426121111576652,2.89120579329468E-19,0.00144640237377705));
#34093=CARTESIAN_POINT('',(0.,0.,0.));
#34094=CARTESIAN_POINT('',(0.00426116004836162,0.,0.00144655281350068));
#34095=CARTESIAN_POINT('',(0.00461939766255643,0.,0.00191341716182545));
#34096=CARTESIAN_POINT('',(0.00461939766255643,0.,0.00191341716182545));
#34097=CARTESIAN_POINT('',(0.00461939766255643,0.,0.00191341716182545));
#34098=CARTESIAN_POINT('',(0.00403596246968851,0.,0.00199022786214689));
#34099=CARTESIAN_POINT('',(0.,0.,0.));
#34100=CARTESIAN_POINT('',(0.00403589220284807,0.,0.00199037034920393));
#34101=CARTESIAN_POINT('',(0.00433012701892219,0.,0.0025));
#34102=CARTESIAN_POINT('',(0.00433012701892219,2.89120579329468E-19,0.0025));
#34103=CARTESIAN_POINT('',(0.00433012701892219,0.,0.0025));
#34104=CARTESIAN_POINT('',(0.00374165738677394,0.,0.0025));
#34105=CARTESIAN_POINT('',(0.,0.,0.));
#34106=CARTESIAN_POINT('',(0.00374156912278306,0.,0.00250013209639738));
#34107=CARTESIAN_POINT('',(0.00396676670145617,0.,0.0030438071450436));
#34108=CARTESIAN_POINT('',(0.00396676670145617,2.89120579329468E-19,0.0030438071450436));
#34109=CARTESIAN_POINT('',(0.00396676670145617,0.,0.0030438071450436));
#34110=CARTESIAN_POINT('',(0.00338333150858826,2.89120579329468E-19,0.00296699644472216));
#34111=CARTESIAN_POINT('',(0.,0.,0.));
#34112=CARTESIAN_POINT('',(0.00338322675766829,0.,0.00296711589025391));
#34113=CARTESIAN_POINT('',(0.00353553390593274,0.,0.00353553390593274));
#34114=CARTESIAN_POINT('',(0.00353553390593274,0.,0.00353553390593274));
#34115=CARTESIAN_POINT('',(0.00353553390593274,0.,0.00353553390593274));
#34116=CARTESIAN_POINT('',(0.00296711589025391,0.,0.00338322675766829));
#34117=CARTESIAN_POINT('',(0.,0.,0.));
#34118=CARTESIAN_POINT('',(0.00296699644472216,0.,0.00338333150858826));
#34119=CARTESIAN_POINT('',(0.0030438071450436,0.,0.00396676670145617));
#34120=CARTESIAN_POINT('',(0.0030438071450436,0.,0.00396676670145617));
#34121=CARTESIAN_POINT('',(0.0030438071450436,0.,0.00396676670145617));
#34122=CARTESIAN_POINT('',(0.00250013209639738,0.,0.00374156912278306));
#34123=CARTESIAN_POINT('',(0.,0.,0.));
#34124=CARTESIAN_POINT('',(0.0025,0.,0.00374165738677394));
#34125=CARTESIAN_POINT('',(0.0025,0.,0.00433012701892219));
#34126=CARTESIAN_POINT('',(0.0025,0.,0.00433012701892219));
#34127=CARTESIAN_POINT('',(0.0025,0.,0.00433012701892219));
#34128=CARTESIAN_POINT('',(0.00199037034920393,0.,0.00403589220284807));
#34129=CARTESIAN_POINT('',(0.,0.,0.));
#34130=CARTESIAN_POINT('',(0.00199022786214689,0.,0.00403596246968851));
#34131=CARTESIAN_POINT('',(0.00191341716182545,0.,0.00461939766255643));
#34132=CARTESIAN_POINT('',(0.00191341716182545,0.,0.00461939766255643));
#34133=CARTESIAN_POINT('',(0.00191341716182545,0.,0.00461939766255643));
#34134=CARTESIAN_POINT('',(0.00144655281350068,0.,0.00426116004836163));
#34135=CARTESIAN_POINT('',(0.,0.,0.));
#34136=CARTESIAN_POINT('',(0.00144640237377705,0.,0.00426121111576652));
#34137=CARTESIAN_POINT('',(0.0012940952255126,0.,0.00482962913144534));
#34138=CARTESIAN_POINT('',(0.0012940952255126,0.,0.00482962913144534));
#34139=CARTESIAN_POINT('',(0.0012940952255126,0.,0.00482962913144534));
#34140=CARTESIAN_POINT('',(0.000877984358098221,2.89120579329468E-19,0.00441351826403096));
#34141=CARTESIAN_POINT('',(0.,0.,0.));
#34142=CARTESIAN_POINT('',(0.000877828539773374,0.,0.00441354925822283));
#34143=CARTESIAN_POINT('',(0.000652630961100259,0.,0.00495722430686905));
#34144=CARTESIAN_POINT('',(0.000652630961100259,2.89120579329468E-19,0.00495722430686905));
#34145=CARTESIAN_POINT('',(0.000652630961100259,0.,0.00495722430686905));
#34146=CARTESIAN_POINT('',(0.000294393346905451,0.,0.00449035995854428));
#34147=CARTESIAN_POINT('',(0.,0.,0.));
#34148=CARTESIAN_POINT('',(0.000294234816074127,0.,0.00449037034920393));
#34149=CARTESIAN_POINT('',(3.06161699786893E-19,0.,0.005));
#34150=CARTESIAN_POINT('',(3.06161699786893E-19,2.89120579329468E-19,0.005));
#34151=CARTESIAN_POINT('',(3.06161699786893E-19,0.,0.005));
#34152=CARTESIAN_POINT('',(-0.000294234816074128,0.,0.00449037034920393));
#34153=CARTESIAN_POINT('',(0.,0.,0.));
#34154=CARTESIAN_POINT('',(-0.00029439334690545,0.,0.00449035995854428));
#34155=CARTESIAN_POINT('',(-0.000652630961100257,0.,0.00495722430686905));
#34156=CARTESIAN_POINT('',(-0.000652630961100257,0.,0.00495722430686905));
#34157=CARTESIAN_POINT('',(-0.000652630961100257,0.,0.00495722430686905));
#34158=CARTESIAN_POINT('',(-0.000877828539773374,0.,0.00441354925822283));
#34159=CARTESIAN_POINT('',(0.,0.,0.));
#34160=CARTESIAN_POINT('',(-0.000877984358098222,0.,0.00441351826403096));
#34161=CARTESIAN_POINT('',(-0.0012940952255126,0.,0.00482962913144534));
#34162=CARTESIAN_POINT('',(-0.0012940952255126,0.,0.00482962913144534));
#34163=CARTESIAN_POINT('',(-0.0012940952255126,0.,0.00482962913144534));
#34164=CARTESIAN_POINT('',(-0.00144640237377705,0.,0.00426121111576652));
#34165=CARTESIAN_POINT('',(0.,0.,0.));
#34166=CARTESIAN_POINT('',(-0.00144655281350068,0.,0.00426116004836162));
#34167=CARTESIAN_POINT('',(-0.00191341716182545,0.,0.00461939766255643));
#34168=CARTESIAN_POINT('',(-0.00191341716182545,0.,0.00461939766255643));
#34169=CARTESIAN_POINT('',(-0.00191341716182545,0.,0.00461939766255643));
#34170=CARTESIAN_POINT('',(-0.00199022786214689,2.16840434497101E-19,0.00403596246968851));
#34171=CARTESIAN_POINT('',(0.,0.,0.));
#34172=CARTESIAN_POINT('',(-0.00199037034920393,0.,0.00403589220284807));
#34173=CARTESIAN_POINT('',(-0.0025,0.,0.00433012701892219));
#34174=CARTESIAN_POINT('',(-0.0025,2.89120579329468E-19,0.00433012701892219));
#34175=CARTESIAN_POINT('',(-0.0025,0.,0.00433012701892219));
#34176=CARTESIAN_POINT('',(-0.0025,0.,0.00374165738677394));
#34177=CARTESIAN_POINT('',(0.,0.,0.));
#34178=CARTESIAN_POINT('',(-0.00250013209639738,0.,0.00374156912278306));
#34179=CARTESIAN_POINT('',(-0.0030438071450436,0.,0.00396676670145617));
#34180=CARTESIAN_POINT('',(-0.0030438071450436,0.,0.00396676670145617));
#34181=CARTESIAN_POINT('',(-0.0030438071450436,0.,0.00396676670145617));
#34182=CARTESIAN_POINT('',(-0.00296699644472215,0.,0.00338333150858826));
#34183=CARTESIAN_POINT('',(0.,0.,0.));
#34184=CARTESIAN_POINT('',(-0.00296711589025392,0.,0.00338322675766829));
#34185=CARTESIAN_POINT('',(-0.00353553390593274,0.,0.00353553390593274));
#34186=CARTESIAN_POINT('',(-0.00353553390593274,0.,0.00353553390593274));
#34187=CARTESIAN_POINT('',(-0.00353553390593274,0.,0.00353553390593274));
#34188=CARTESIAN_POINT('',(-0.00338322675766829,0.,0.00296711589025391));
#34189=CARTESIAN_POINT('',(0.,0.,0.));
#34190=CARTESIAN_POINT('',(-0.00338333150858826,0.,0.00296699644472216));
#34191=CARTESIAN_POINT('',(-0.00396676670145617,0.,0.0030438071450436));
#34192=CARTESIAN_POINT('',(-0.00396676670145617,0.,0.0030438071450436));
#34193=CARTESIAN_POINT('',(-0.00396676670145617,0.,0.0030438071450436));
#34194=CARTESIAN_POINT('',(-0.00374156912278306,0.,0.00250013209639738));
#34195=CARTESIAN_POINT('',(0.,0.,0.));
#34196=CARTESIAN_POINT('',(-0.00374165738677394,0.,0.0025));
#34197=CARTESIAN_POINT('',(-0.00433012701892219,0.,0.0025));
#34198=CARTESIAN_POINT('',(-0.00433012701892219,0.,0.0025));
#34199=CARTESIAN_POINT('',(-0.00433012701892219,0.,0.0025));
#34200=CARTESIAN_POINT('',(-0.00403589220284807,0.,0.00199037034920393));
#34201=CARTESIAN_POINT('',(0.,0.,0.));
#34202=CARTESIAN_POINT('',(-0.00403596246968851,0.,0.00199022786214689));
#34203=CARTESIAN_POINT('',(-0.00461939766255643,0.,0.00191341716182545));
#34204=CARTESIAN_POINT('',(-0.00461939766255643,0.,0.00191341716182545));
#34205=CARTESIAN_POINT('',(-0.00461939766255643,0.,0.00191341716182545));
#34206=CARTESIAN_POINT('',(-0.00426116004836163,0.,0.00144655281350068));
#34207=CARTESIAN_POINT('',(0.,0.,0.));
#34208=CARTESIAN_POINT('',(-0.00426121111576652,0.,0.00144640237377705));
#34209=CARTESIAN_POINT('',(-0.00482962913144534,0.,0.0012940952255126));
#34210=CARTESIAN_POINT('',(-0.00482962913144534,0.,0.0012940952255126));
#34211=CARTESIAN_POINT('',(-0.00482962913144534,0.,0.0012940952255126));
#34212=CARTESIAN_POINT('',(-0.00441351826403096,2.89120579329468E-19,0.000877984358098221));
#34213=CARTESIAN_POINT('',(0.,0.,0.));
#34214=CARTESIAN_POINT('',(-0.00441354925822283,0.,0.000877828539773374));
#34215=CARTESIAN_POINT('',(-0.00495722430686905,0.,0.00065263096110026));
#34216=CARTESIAN_POINT('',(-0.00495722430686905,0.,0.00065263096110026));
#34217=CARTESIAN_POINT('',(-0.00495722430686905,0.,0.00065263096110026));
#34218=CARTESIAN_POINT('',(-0.00449035995854428,0.,0.000294393346905453));
#34219=CARTESIAN_POINT('',(0.,0.,0.));
#34220=CARTESIAN_POINT('',(-0.00449037034920393,0.,0.000294234816074127));
#34221=CARTESIAN_POINT('',(-0.005,0.,6.12323399573786E-19));
#34222=CARTESIAN_POINT('',(-0.005,0.,6.12323399573786E-19));
#34223=CARTESIAN_POINT('',(-0.005,0.,6.12323399573786E-19));
#34224=CARTESIAN_POINT('',(-0.00449037034920393,0.,-0.000294234816074128));
#34225=CARTESIAN_POINT('',(0.,0.,0.));
#34226=CARTESIAN_POINT('',(-0.00449035995854428,0.,-0.000294393346905449));
#34227=CARTESIAN_POINT('',(-0.00495722430686905,0.,-0.000652630961100257));
#34228=CARTESIAN_POINT('',(-0.00495722430686905,0.,-0.000652630961100257));
#34229=CARTESIAN_POINT('',(-0.00495722430686905,0.,-0.000652630961100257));
#34230=CARTESIAN_POINT('',(-0.00441354925822283,0.,-0.000877828539773374));
#34231=CARTESIAN_POINT('',(0.,0.,0.));
#34232=CARTESIAN_POINT('',(-0.00441351826403096,0.,-0.000877984358098219));
#34233=CARTESIAN_POINT('',(-0.00482962913144534,0.,-0.0012940952255126));
#34234=CARTESIAN_POINT('',(-0.00482962913144534,2.89120579329468E-19,-0.0012940952255126));
#34235=CARTESIAN_POINT('',(-0.00482962913144534,0.,-0.0012940952255126));
#34236=CARTESIAN_POINT('',(-0.00426121111576652,0.,-0.00144640237377705));
#34237=CARTESIAN_POINT('',(0.,0.,0.));
#34238=CARTESIAN_POINT('',(-0.00426116004836163,0.,-0.00144655281350068));
#34239=CARTESIAN_POINT('',(-0.00461939766255644,0.,-0.00191341716182544));
#34240=CARTESIAN_POINT('',(-0.00461939766255644,0.,-0.00191341716182544));
#34241=CARTESIAN_POINT('',(-0.00461939766255644,0.,-0.00191341716182544));
#34242=CARTESIAN_POINT('',(-0.00403596246968851,0.,-0.00199022786214689));
#34243=CARTESIAN_POINT('',(0.,0.,0.));
#34244=CARTESIAN_POINT('',(-0.00403589220284807,0.,-0.00199037034920393));
#34245=CARTESIAN_POINT('',(-0.00433012701892219,0.,-0.0025));
#34246=CARTESIAN_POINT('',(-0.00433012701892219,2.89120579329468E-19,-0.0025));
#34247=CARTESIAN_POINT('',(-0.00433012701892219,0.,-0.0025));
#34248=CARTESIAN_POINT('',(-0.00374165738677394,0.,-0.0025));
#34249=CARTESIAN_POINT('',(0.,0.,0.));
#34250=CARTESIAN_POINT('',(-0.00374156912278306,0.,-0.00250013209639738));
#34251=CARTESIAN_POINT('',(-0.00396676670145617,0.,-0.0030438071450436));
#34252=CARTESIAN_POINT('',(-0.00396676670145617,0.,-0.0030438071450436));
#34253=CARTESIAN_POINT('',(-0.00396676670145617,0.,-0.0030438071450436));
#34254=CARTESIAN_POINT('',(-0.00338333150858826,0.,-0.00296699644472216));
#34255=CARTESIAN_POINT('',(0.,0.,0.));
#34256=CARTESIAN_POINT('',(-0.00338322675766829,0.,-0.00296711589025391));
#34257=CARTESIAN_POINT('',(-0.00353553390593274,0.,-0.00353553390593274));
#34258=CARTESIAN_POINT('',(-0.00353553390593274,0.,-0.00353553390593274));
#34259=CARTESIAN_POINT('',(-0.00353553390593274,0.,-0.00353553390593274));
#34260=CARTESIAN_POINT('',(-0.00296711589025391,0.,-0.00338322675766829));
#34261=CARTESIAN_POINT('',(0.,0.,0.));
#34262=CARTESIAN_POINT('',(-0.00296699644472216,0.,-0.00338333150858826));
#34263=CARTESIAN_POINT('',(-0.0030438071450436,0.,-0.00396676670145617));
#34264=CARTESIAN_POINT('',(-0.0030438071450436,0.,-0.00396676670145617));
#34265=CARTESIAN_POINT('',(-0.0030438071450436,0.,-0.00396676670145617));
#34266=CARTESIAN_POINT('',(-0.00250013209639738,0.,-0.00374156912278306));
#34267=CARTESIAN_POINT('',(0.,0.,0.));
#34268=CARTESIAN_POINT('',(-0.0025,0.,-0.00374165738677394));
#34269=CARTESIAN_POINT('',(-0.0025,0.,-0.00433012701892219));
#34270=CARTESIAN_POINT('',(-0.0025,0.,-0.00433012701892219));
#34271=CARTESIAN_POINT('',(-0.0025,0.,-0.00433012701892219));
#34272=CARTESIAN_POINT('',(-0.00199037034920393,0.,-0.00403589220284807));
#34273=CARTESIAN_POINT('',(0.,0.,0.));
#34274=CARTESIAN_POINT('',(-0.0019902278621469,0.,-0.00403596246968851));
#34275=CARTESIAN_POINT('',(-0.00191341716182545,0.,-0.00461939766255643));
#34276=CARTESIAN_POINT('',(-0.00191341716182545,0.,-0.00461939766255643));
#34277=CARTESIAN_POINT('',(-0.00191341716182545,0.,-0.00461939766255643));
#34278=CARTESIAN_POINT('',(-0.00144655281350068,0.,-0.00426116004836162));
#34279=CARTESIAN_POINT('',(0.,0.,0.));
#34280=CARTESIAN_POINT('',(-0.00144640237377705,0.,-0.00426121111576652));
#34281=CARTESIAN_POINT('',(-0.00129409522551261,0.,-0.00482962913144534));
#34282=CARTESIAN_POINT('',(-0.00129409522551261,0.,-0.00482962913144534));
#34283=CARTESIAN_POINT('',(-0.00129409522551261,0.,-0.00482962913144534));
#34284=CARTESIAN_POINT('',(-0.000877984358098223,0.,-0.00441351826403096));
#34285=CARTESIAN_POINT('',(0.,0.,0.));
#34286=CARTESIAN_POINT('',(-0.000877828539773377,0.,-0.00441354925822283));
#34287=CARTESIAN_POINT('',(-0.000652630961100263,0.,-0.00495722430686905));
#34288=CARTESIAN_POINT('',(-0.000652630961100263,0.,-0.00495722430686905));
#34289=CARTESIAN_POINT('',(-0.000652630961100263,0.,-0.00495722430686905));
#34290=CARTESIAN_POINT('',(-0.000294393346905453,0.,-0.00449035995854428));
#34291=CARTESIAN_POINT('',(0.,0.,0.));
#34292=CARTESIAN_POINT('',(-0.000294234816074127,0.,-0.00449037034920393));
#34293=CARTESIAN_POINT('',(-9.18485099360482E-19,0.,-0.005));
#34294=CARTESIAN_POINT('',(-9.18485099360482E-19,0.,-0.005));
#34295=CARTESIAN_POINT('',(-9.18485099360482E-19,0.,-0.005));
#34296=CARTESIAN_POINT('',(0.000294234816074127,0.,-0.00449037034920393));
#34297=CARTESIAN_POINT('',(0.,0.,0.));
#34298=CARTESIAN_POINT('',(0.00029439334690545,0.,-0.00449035995854428));
#34299=CARTESIAN_POINT('',(0.000652630961100256,0.,-0.00495722430686905));
#34300=CARTESIAN_POINT('',(0.000652630961100256,0.,-0.00495722430686905));
#34301=CARTESIAN_POINT('',(0.000652630961100256,0.,-0.00495722430686905));
#34302=CARTESIAN_POINT('',(0.000877828539773373,0.,-0.00441354925822283));
#34303=CARTESIAN_POINT('',(0.,0.,0.));
#34304=CARTESIAN_POINT('',(0.000877984358098219,0.,-0.00441351826403096));
#34305=CARTESIAN_POINT('',(0.0012940952255126,0.,-0.00482962913144534));
#34306=CARTESIAN_POINT('',(0.0012940952255126,0.,-0.00482962913144534));
#34307=CARTESIAN_POINT('',(0.0012940952255126,0.,-0.00482962913144534));
#34308=CARTESIAN_POINT('',(0.00144640237377704,1.44560289664734E-19,-0.00426121111576652));
#34309=CARTESIAN_POINT('',(0.,0.,0.));
#34310=CARTESIAN_POINT('',(0.00144655281350067,0.,-0.00426116004836163));
#34311=CARTESIAN_POINT('',(0.00191341716182544,0.,-0.00461939766255644));
#34312=CARTESIAN_POINT('',(0.00191341716182544,0.,-0.00461939766255644));
#34313=CARTESIAN_POINT('',(0.00191341716182544,0.,-0.00461939766255644));
#34314=CARTESIAN_POINT('',(0.00199022786214689,0.,-0.00403596246968851));
#34315=CARTESIAN_POINT('',(0.,0.,0.));
#34316=CARTESIAN_POINT('',(0.00199037034920392,0.,-0.00403589220284807));
#34317=CARTESIAN_POINT('',(0.0025,0.,-0.00433012701892219));
#34318=CARTESIAN_POINT('',(0.0025,0.,-0.00433012701892219));
#34319=CARTESIAN_POINT('',(0.0025,0.,-0.00433012701892219));
#34320=CARTESIAN_POINT('',(0.0025,0.,-0.00374165738677394));
#34321=CARTESIAN_POINT('',(0.,0.,0.));
#34322=CARTESIAN_POINT('',(0.00250013209639738,0.,-0.00374156912278307));
#34323=CARTESIAN_POINT('',(0.0030438071450436,0.,-0.00396676670145618));
#34324=CARTESIAN_POINT('',(0.0030438071450436,2.89120579329468E-19,-0.00396676670145618));
#34325=CARTESIAN_POINT('',(0.0030438071450436,0.,-0.00396676670145618));
#34326=CARTESIAN_POINT('',(0.00296699644472215,0.,-0.00338333150858826));
#34327=CARTESIAN_POINT('',(0.,0.,0.));
#34328=CARTESIAN_POINT('',(0.00296711589025391,0.,-0.00338322675766829));
#34329=CARTESIAN_POINT('',(0.00353553390593274,0.,-0.00353553390593274));
#34330=CARTESIAN_POINT('',(0.00353553390593274,0.,-0.00353553390593274));
#34331=CARTESIAN_POINT('',(0.00353553390593274,0.,-0.00353553390593274));
#34332=CARTESIAN_POINT('',(0.00338322675766829,0.,-0.00296711589025392));
#34333=CARTESIAN_POINT('',(0.,0.,0.));
#34334=CARTESIAN_POINT('',(0.00338333150858826,0.,-0.00296699644472216));
#34335=CARTESIAN_POINT('',(0.00396676670145617,0.,-0.0030438071450436));
#34336=CARTESIAN_POINT('',(0.00396676670145617,0.,-0.0030438071450436));
#34337=CARTESIAN_POINT('',(0.00396676670145617,0.,-0.0030438071450436));
#34338=CARTESIAN_POINT('',(0.00374165738677394,0.,-0.0025));
#34339=CARTESIAN_POINT('',(0.00433012701892219,0.,-0.0025));
#34340=CARTESIAN_POINT('',(0.00433012701892219,0.,-0.0025));
#34341=CARTESIAN_POINT('',(0.00433012701892219,0.,-0.0025));
#34342=CARTESIAN_POINT('',(0.00403589220284806,0.,-0.00199037034920393));
#34343=CARTESIAN_POINT('',(0.,0.,0.));
#34344=CARTESIAN_POINT('',(0.00403596246968851,0.,-0.0019902278621469));
#34345=CARTESIAN_POINT('',(0.00461939766255643,0.,-0.00191341716182545));
#34346=CARTESIAN_POINT('',(0.00461939766255643,0.,-0.00191341716182545));
#34347=CARTESIAN_POINT('',(0.00461939766255643,0.,-0.00191341716182545));
#34348=CARTESIAN_POINT('',(0.00426116004836162,0.,-0.00144655281350068));
#34349=CARTESIAN_POINT('',(0.,0.,0.));
#34350=CARTESIAN_POINT('',(0.00426121111576652,0.,-0.00144640237377705));
#34351=CARTESIAN_POINT('',(0.00482962913144534,0.,-0.00129409522551261));
#34352=CARTESIAN_POINT('',(0.00482962913144534,2.89120579329468E-19,-0.00129409522551261));
#34353=CARTESIAN_POINT('',(0.00482962913144534,0.,-0.00129409522551261));
#34354=CARTESIAN_POINT('',(0.00441351826403096,2.89120579329468E-19,-0.000877984358098224));
#34355=CARTESIAN_POINT('',(0.,0.,0.));
#34356=CARTESIAN_POINT('',(0.00441354925822283,0.,-0.000877828539773378));
#34357=CARTESIAN_POINT('',(0.00495722430686905,0.,-0.000652630961100263));
#34358=CARTESIAN_POINT('',(0.00495722430686905,0.,-0.000652630961100263));
#34359=CARTESIAN_POINT('',(0.00495722430686905,0.,-0.000652630961100263));
#34360=CARTESIAN_POINT('',(0.00449035995854428,0.,-0.000294393346905455));
#34361=CARTESIAN_POINT('',(0.,0.,0.));
#34362=CARTESIAN_POINT('',(0.00449037034920393,0.,-0.000294234816074128));
#34363=CARTESIAN_POINT('',(0.005,0.,0.));
#34364=CARTESIAN_POINT('',(0.,0.,0.));
#34365=CARTESIAN_POINT('',(0.,0.,-0.00025));
#34366=CARTESIAN_POINT('',(0.,0.004,0.));
#34367=CARTESIAN_POINT('',(0.005,0.004,0.));
#34368=CARTESIAN_POINT('',(0.00449037034920393,0.004,0.000294234816074125));
#34369=CARTESIAN_POINT('',(0.005,0.004,0.));
#34370=CARTESIAN_POINT('',(0.005,0.004,0.));
#34371=CARTESIAN_POINT('',(0.00449037034920393,0.004,-0.000294234816074128));
#34372=CARTESIAN_POINT('',(0.,0.004,0.));
#34373=CARTESIAN_POINT('',(0.00449035995854428,0.004,-0.000294393346905455));
#34374=CARTESIAN_POINT('',(0.00495722430686905,0.004,-0.000652630961100263));
#34375=CARTESIAN_POINT('',(0.00495722430686905,0.004,-0.000652630961100263));
#34376=CARTESIAN_POINT('',(0.00495722430686905,0.004,-0.000652630961100263));
#34377=CARTESIAN_POINT('',(0.00441354925822283,0.004,-0.000877828539773378));
#34378=CARTESIAN_POINT('',(0.,0.004,0.));
#34379=CARTESIAN_POINT('',(0.00441351826403096,0.004,-0.000877984358098224));
#34380=CARTESIAN_POINT('',(0.00482962913144534,0.004,-0.00129409522551261));
#34381=CARTESIAN_POINT('',(0.00482962913144534,0.004,-0.00129409522551261));
#34382=CARTESIAN_POINT('',(0.00482962913144534,0.004,-0.00129409522551261));
#34383=CARTESIAN_POINT('',(0.00426121111576652,0.004,-0.00144640237377705));
#34384=CARTESIAN_POINT('',(0.,0.004,0.));
#34385=CARTESIAN_POINT('',(0.00426116004836162,0.004,-0.00144655281350068));
#34386=CARTESIAN_POINT('',(0.00461939766255643,0.004,-0.00191341716182545));
#34387=CARTESIAN_POINT('',(0.00461939766255643,0.004,-0.00191341716182545));
#34388=CARTESIAN_POINT('',(0.00461939766255643,0.004,-0.00191341716182545));
#34389=CARTESIAN_POINT('',(0.00403596246968851,0.004,-0.0019902278621469));
#34390=CARTESIAN_POINT('',(0.,0.004,0.));
#34391=CARTESIAN_POINT('',(0.00403589220284806,0.004,-0.00199037034920393));
#34392=CARTESIAN_POINT('',(0.00433012701892219,0.004,-0.0025));
#34393=CARTESIAN_POINT('',(0.00433012701892219,0.004,-0.0025));
#34394=CARTESIAN_POINT('',(0.00433012701892219,0.004,-0.0025));
#34395=CARTESIAN_POINT('',(0.00374165738677394,0.004,-0.0025));
#34396=CARTESIAN_POINT('',(0.00396676670145617,0.004,-0.0030438071450436));
#34397=CARTESIAN_POINT('',(0.00396676670145617,0.004,-0.0030438071450436));
#34398=CARTESIAN_POINT('',(0.00396676670145617,0.004,-0.0030438071450436));
#34399=CARTESIAN_POINT('',(0.00338333150858826,0.004,-0.00296699644472216));
#34400=CARTESIAN_POINT('',(0.,0.004,0.));
#34401=CARTESIAN_POINT('',(0.00338322675766829,0.004,-0.00296711589025392));
#34402=CARTESIAN_POINT('',(0.00353553390593274,0.004,-0.00353553390593274));
#34403=CARTESIAN_POINT('',(0.00353553390593274,0.004,-0.00353553390593274));
#34404=CARTESIAN_POINT('',(0.00353553390593274,0.004,-0.00353553390593274));
#34405=CARTESIAN_POINT('',(0.00296711589025391,0.004,-0.00338322675766829));
#34406=CARTESIAN_POINT('',(0.,0.004,0.));
#34407=CARTESIAN_POINT('',(0.00296699644472215,0.004,-0.00338333150858826));
#34408=CARTESIAN_POINT('',(0.0030438071450436,0.004,-0.00396676670145618));
#34409=CARTESIAN_POINT('',(0.0030438071450436,0.004,-0.00396676670145618));
#34410=CARTESIAN_POINT('',(0.0030438071450436,0.004,-0.00396676670145618));
#34411=CARTESIAN_POINT('',(0.00250013209639738,0.004,-0.00374156912278307));
#34412=CARTESIAN_POINT('',(0.,0.004,0.));
#34413=CARTESIAN_POINT('',(0.0025,0.004,-0.00374165738677394));
#34414=CARTESIAN_POINT('',(0.0025,0.004,-0.00433012701892219));
#34415=CARTESIAN_POINT('',(0.0025,0.004,-0.00433012701892219));
#34416=CARTESIAN_POINT('',(0.0025,0.004,-0.00433012701892219));
#34417=CARTESIAN_POINT('',(0.00199037034920392,0.004,-0.00403589220284807));
#34418=CARTESIAN_POINT('',(0.,0.004,0.));
#34419=CARTESIAN_POINT('',(0.00199022786214689,0.004,-0.00403596246968851));
#34420=CARTESIAN_POINT('',(0.00191341716182544,0.004,-0.00461939766255644));
#34421=CARTESIAN_POINT('',(0.00191341716182544,0.004,-0.00461939766255644));
#34422=CARTESIAN_POINT('',(0.00191341716182544,0.004,-0.00461939766255644));
#34423=CARTESIAN_POINT('',(0.00144655281350068,0.004,-0.00426116004836163));
#34424=CARTESIAN_POINT('',(0.,0.004,0.));
#34425=CARTESIAN_POINT('',(0.00144640237377704,0.004,-0.00426121111576652));
#34426=CARTESIAN_POINT('',(0.0012940952255126,0.004,-0.00482962913144534));
#34427=CARTESIAN_POINT('',(0.0012940952255126,0.004,-0.00482962913144534));
#34428=CARTESIAN_POINT('',(0.0012940952255126,0.004,-0.00482962913144534));
#34429=CARTESIAN_POINT('',(0.000877984358098219,0.004,-0.00441351826403096));
#34430=CARTESIAN_POINT('',(0.,0.004,0.));
#34431=CARTESIAN_POINT('',(0.000877828539773373,0.004,-0.00441354925822283));
#34432=CARTESIAN_POINT('',(0.000652630961100256,0.004,-0.00495722430686905));
#34433=CARTESIAN_POINT('',(0.000652630961100256,0.004,-0.00495722430686905));
#34434=CARTESIAN_POINT('',(0.000652630961100256,0.004,-0.00495722430686905));
#34435=CARTESIAN_POINT('',(0.00029439334690545,0.004,-0.00449035995854428));
#34436=CARTESIAN_POINT('',(0.,0.004,0.));
#34437=CARTESIAN_POINT('',(0.000294234816074127,0.004,-0.00449037034920393));
#34438=CARTESIAN_POINT('',(-9.18485099360482E-19,0.004,-0.005));
#34439=CARTESIAN_POINT('',(-9.18485099360482E-19,0.004,-0.005));
#34440=CARTESIAN_POINT('',(-9.18485099360482E-19,0.004,-0.005));
#34441=CARTESIAN_POINT('',(-0.000294234816074127,0.004,-0.00449037034920393));
#34442=CARTESIAN_POINT('',(0.,0.004,0.));
#34443=CARTESIAN_POINT('',(-0.000294393346905453,0.004,-0.00449035995854428));
#34444=CARTESIAN_POINT('',(-0.000652630961100263,0.004,-0.00495722430686905));
#34445=CARTESIAN_POINT('',(-0.000652630961100263,0.004,-0.00495722430686905));
#34446=CARTESIAN_POINT('',(-0.000652630961100263,0.004,-0.00495722430686905));
#34447=CARTESIAN_POINT('',(-0.000877828539773377,0.004,-0.00441354925822283));
#34448=CARTESIAN_POINT('',(0.,0.004,0.));
#34449=CARTESIAN_POINT('',(-0.000877984358098223,0.004,-0.00441351826403096));
#34450=CARTESIAN_POINT('',(-0.00129409522551261,0.004,-0.00482962913144534));
#34451=CARTESIAN_POINT('',(-0.00129409522551261,0.004,-0.00482962913144534));
#34452=CARTESIAN_POINT('',(-0.00129409522551261,0.004,-0.00482962913144534));
#34453=CARTESIAN_POINT('',(-0.00144640237377705,0.004,-0.00426121111576652));
#34454=CARTESIAN_POINT('',(0.,0.004,0.));
#34455=CARTESIAN_POINT('',(-0.00144655281350068,0.004,-0.00426116004836162));
#34456=CARTESIAN_POINT('',(-0.00191341716182545,0.004,-0.00461939766255643));
#34457=CARTESIAN_POINT('',(-0.00191341716182545,0.004,-0.00461939766255643));
#34458=CARTESIAN_POINT('',(-0.00191341716182545,0.004,-0.00461939766255643));
#34459=CARTESIAN_POINT('',(-0.0019902278621469,0.004,-0.00403596246968851));
#34460=CARTESIAN_POINT('',(0.,0.004,0.));
#34461=CARTESIAN_POINT('',(-0.00199037034920393,0.004,-0.00403589220284807));
#34462=CARTESIAN_POINT('',(-0.0025,0.004,-0.00433012701892219));
#34463=CARTESIAN_POINT('',(-0.0025,0.004,-0.00433012701892219));
#34464=CARTESIAN_POINT('',(-0.0025,0.004,-0.00433012701892219));
#34465=CARTESIAN_POINT('',(-0.0025,0.004,-0.00374165738677394));
#34466=CARTESIAN_POINT('',(0.,0.004,0.));
#34467=CARTESIAN_POINT('',(-0.00250013209639738,0.004,-0.00374156912278306));
#34468=CARTESIAN_POINT('',(-0.0030438071450436,0.004,-0.00396676670145617));
#34469=CARTESIAN_POINT('',(-0.0030438071450436,0.004,-0.00396676670145617));
#34470=CARTESIAN_POINT('',(-0.0030438071450436,0.004,-0.00396676670145617));
#34471=CARTESIAN_POINT('',(-0.00296699644472216,0.004,-0.00338333150858826));
#34472=CARTESIAN_POINT('',(0.,0.004,0.));
#34473=CARTESIAN_POINT('',(-0.00296711589025392,0.004,-0.00338322675766829));
#34474=CARTESIAN_POINT('',(-0.00353553390593274,0.004,-0.00353553390593274));
#34475=CARTESIAN_POINT('',(-0.00353553390593274,0.004,-0.00353553390593274));
#34476=CARTESIAN_POINT('',(-0.00353553390593274,0.004,-0.00353553390593274));
#34477=CARTESIAN_POINT('',(-0.0033832267576683,0.004,-0.00296711589025391));
#34478=CARTESIAN_POINT('',(0.,0.004,0.));
#34479=CARTESIAN_POINT('',(-0.00338333150858826,0.004,-0.00296699644472216));
#34480=CARTESIAN_POINT('',(-0.00396676670145617,0.004,-0.0030438071450436));
#34481=CARTESIAN_POINT('',(-0.00396676670145617,0.004,-0.0030438071450436));
#34482=CARTESIAN_POINT('',(-0.00396676670145617,0.004,-0.0030438071450436));
#34483=CARTESIAN_POINT('',(-0.00374156912278306,0.004,-0.00250013209639738));
#34484=CARTESIAN_POINT('',(0.,0.004,0.));
#34485=CARTESIAN_POINT('',(-0.00374165738677394,0.004,-0.0025));
#34486=CARTESIAN_POINT('',(-0.00433012701892219,0.004,-0.0025));
#34487=CARTESIAN_POINT('',(-0.00433012701892219,0.004,-0.0025));
#34488=CARTESIAN_POINT('',(-0.00433012701892219,0.004,-0.0025));
#34489=CARTESIAN_POINT('',(-0.00403589220284807,0.004,-0.00199037034920393));
#34490=CARTESIAN_POINT('',(0.,0.004,0.));
#34491=CARTESIAN_POINT('',(-0.00403596246968851,0.004,-0.00199022786214689));
#34492=CARTESIAN_POINT('',(-0.00461939766255644,0.004,-0.00191341716182544));
#34493=CARTESIAN_POINT('',(-0.00461939766255644,0.004,-0.00191341716182544));
#34494=CARTESIAN_POINT('',(-0.00461939766255644,0.004,-0.00191341716182544));
#34495=CARTESIAN_POINT('',(-0.00426116004836163,0.004,-0.00144655281350068));
#34496=CARTESIAN_POINT('',(0.,0.004,0.));
#34497=CARTESIAN_POINT('',(-0.00426121111576652,0.004,-0.00144640237377705));
#34498=CARTESIAN_POINT('',(-0.00482962913144534,0.004,-0.0012940952255126));
#34499=CARTESIAN_POINT('',(-0.00482962913144534,0.004,-0.0012940952255126));
#34500=CARTESIAN_POINT('',(-0.00482962913144534,0.004,-0.0012940952255126));
#34501=CARTESIAN_POINT('',(-0.00441351826403096,0.004,-0.00087798435809822));
#34502=CARTESIAN_POINT('',(0.,0.004,0.));
#34503=CARTESIAN_POINT('',(-0.00441354925822283,0.004,-0.000877828539773374));
#34504=CARTESIAN_POINT('',(-0.00495722430686905,0.004,-0.000652630961100257));
#34505=CARTESIAN_POINT('',(-0.00495722430686905,0.004,-0.000652630961100257));
#34506=CARTESIAN_POINT('',(-0.00495722430686905,0.004,-0.000652630961100257));
#34507=CARTESIAN_POINT('',(-0.00449035995854428,0.004,-0.00029439334690545));
#34508=CARTESIAN_POINT('',(0.,0.004,0.));
#34509=CARTESIAN_POINT('',(-0.00449037034920393,0.004,-0.000294234816074128));
#34510=CARTESIAN_POINT('',(-0.005,0.004,6.12323399573786E-19));
#34511=CARTESIAN_POINT('',(-0.005,0.004,6.12323399573786E-19));
#34512=CARTESIAN_POINT('',(-0.005,0.004,6.12323399573786E-19));
#34513=CARTESIAN_POINT('',(-0.00449037034920393,0.004,0.000294234816074127));
#34514=CARTESIAN_POINT('',(0.,0.004,0.));
#34515=CARTESIAN_POINT('',(-0.00449035995854428,0.004,0.000294393346905453));
#34516=CARTESIAN_POINT('',(-0.00495722430686905,0.004,0.00065263096110026));
#34517=CARTESIAN_POINT('',(-0.00495722430686905,0.004,0.00065263096110026));
#34518=CARTESIAN_POINT('',(-0.00495722430686905,0.004,0.00065263096110026));
#34519=CARTESIAN_POINT('',(-0.00441354925822283,0.004,0.000877828539773374));
#34520=CARTESIAN_POINT('',(0.,0.004,0.));
#34521=CARTESIAN_POINT('',(-0.00441351826403096,0.004,0.000877984358098221));
#34522=CARTESIAN_POINT('',(-0.00482962913144534,0.004,0.0012940952255126));
#34523=CARTESIAN_POINT('',(-0.00482962913144534,0.004,0.0012940952255126));
#34524=CARTESIAN_POINT('',(-0.00482962913144534,0.004,0.0012940952255126));
#34525=CARTESIAN_POINT('',(-0.00426121111576652,0.004,0.00144640237377705));
#34526=CARTESIAN_POINT('',(0.,0.004,0.));
#34527=CARTESIAN_POINT('',(-0.00426116004836163,0.004,0.00144655281350068));
#34528=CARTESIAN_POINT('',(-0.00461939766255643,0.004,0.00191341716182545));
#34529=CARTESIAN_POINT('',(-0.00461939766255643,0.004,0.00191341716182545));
#34530=CARTESIAN_POINT('',(-0.00461939766255643,0.004,0.00191341716182545));
#34531=CARTESIAN_POINT('',(-0.00403596246968851,0.004,0.00199022786214689));
#34532=CARTESIAN_POINT('',(0.,0.004,0.));
#34533=CARTESIAN_POINT('',(-0.00403589220284807,0.004,0.00199037034920393));
#34534=CARTESIAN_POINT('',(-0.00433012701892219,0.004,0.0025));
#34535=CARTESIAN_POINT('',(-0.00433012701892219,0.004,0.0025));
#34536=CARTESIAN_POINT('',(-0.00433012701892219,0.004,0.0025));
#34537=CARTESIAN_POINT('',(-0.00374165738677394,0.004,0.0025));
#34538=CARTESIAN_POINT('',(0.,0.004,0.));
#34539=CARTESIAN_POINT('',(-0.00374156912278306,0.004,0.00250013209639738));
#34540=CARTESIAN_POINT('',(-0.00396676670145617,0.004,0.0030438071450436));
#34541=CARTESIAN_POINT('',(-0.00396676670145617,0.004,0.0030438071450436));
#34542=CARTESIAN_POINT('',(-0.00396676670145617,0.004,0.0030438071450436));
#34543=CARTESIAN_POINT('',(-0.00338333150858826,0.004,0.00296699644472216));
#34544=CARTESIAN_POINT('',(0.,0.004,0.));
#34545=CARTESIAN_POINT('',(-0.00338322675766829,0.004,0.00296711589025391));
#34546=CARTESIAN_POINT('',(-0.00353553390593274,0.004,0.00353553390593274));
#34547=CARTESIAN_POINT('',(-0.00353553390593274,0.004,0.00353553390593274));
#34548=CARTESIAN_POINT('',(-0.00353553390593274,0.004,0.00353553390593274));
#34549=CARTESIAN_POINT('',(-0.00296711589025392,0.004,0.00338322675766829));
#34550=CARTESIAN_POINT('',(0.,0.004,0.));
#34551=CARTESIAN_POINT('',(-0.00296699644472215,0.004,0.00338333150858826));
#34552=CARTESIAN_POINT('',(-0.0030438071450436,0.004,0.00396676670145617));
#34553=CARTESIAN_POINT('',(-0.0030438071450436,0.004,0.00396676670145617));
#34554=CARTESIAN_POINT('',(-0.0030438071450436,0.004,0.00396676670145617));
#34555=CARTESIAN_POINT('',(-0.00250013209639738,0.004,0.00374156912278307));
#34556=CARTESIAN_POINT('',(0.,0.004,0.));
#34557=CARTESIAN_POINT('',(-0.0025,0.004,0.00374165738677394));
#34558=CARTESIAN_POINT('',(-0.0025,0.004,0.00433012701892219));
#34559=CARTESIAN_POINT('',(-0.0025,0.004,0.00433012701892219));
#34560=CARTESIAN_POINT('',(-0.0025,0.004,0.00433012701892219));
#34561=CARTESIAN_POINT('',(-0.00199037034920393,0.004,0.00403589220284807));
#34562=CARTESIAN_POINT('',(0.,0.004,0.));
#34563=CARTESIAN_POINT('',(-0.00199022786214689,0.004,0.00403596246968851));
#34564=CARTESIAN_POINT('',(-0.00191341716182545,0.004,0.00461939766255643));
#34565=CARTESIAN_POINT('',(-0.00191341716182545,0.004,0.00461939766255643));
#34566=CARTESIAN_POINT('',(-0.00191341716182545,0.004,0.00461939766255643));
#34567=CARTESIAN_POINT('',(-0.00144655281350068,0.004,0.00426116004836162));
#34568=CARTESIAN_POINT('',(0.,0.004,0.));
#34569=CARTESIAN_POINT('',(-0.00144640237377705,0.004,0.00426121111576652));
#34570=CARTESIAN_POINT('',(-0.0012940952255126,0.004,0.00482962913144534));
#34571=CARTESIAN_POINT('',(-0.0012940952255126,0.004,0.00482962913144534));
#34572=CARTESIAN_POINT('',(-0.0012940952255126,0.004,0.00482962913144534));
#34573=CARTESIAN_POINT('',(-0.000877984358098222,0.004,0.00441351826403096));
#34574=CARTESIAN_POINT('',(0.,0.004,0.));
#34575=CARTESIAN_POINT('',(-0.000877828539773373,0.004,0.00441354925822283));
#34576=CARTESIAN_POINT('',(-0.000652630961100257,0.004,0.00495722430686905));
#34577=CARTESIAN_POINT('',(-0.000652630961100257,0.004,0.00495722430686905));
#34578=CARTESIAN_POINT('',(-0.000652630961100257,0.004,0.00495722430686905));
#34579=CARTESIAN_POINT('',(-0.00029439334690545,0.004,0.00449035995854428));
#34580=CARTESIAN_POINT('',(0.,0.004,0.));
#34581=CARTESIAN_POINT('',(-0.000294234816074128,0.004,0.00449037034920393));
#34582=CARTESIAN_POINT('',(3.06161699786893E-19,0.004,0.005));
#34583=CARTESIAN_POINT('',(3.06161699786893E-19,0.004,0.005));
#34584=CARTESIAN_POINT('',(3.06161699786893E-19,0.004,0.005));
#34585=CARTESIAN_POINT('',(0.000294234816074127,0.004,0.00449037034920393));
#34586=CARTESIAN_POINT('',(0.,0.004,0.));
#34587=CARTESIAN_POINT('',(0.000294393346905452,0.004,0.00449035995854428));
#34588=CARTESIAN_POINT('',(0.000652630961100259,0.004,0.00495722430686905));
#34589=CARTESIAN_POINT('',(0.000652630961100259,0.004,0.00495722430686905));
#34590=CARTESIAN_POINT('',(0.000652630961100259,0.004,0.00495722430686905));
#34591=CARTESIAN_POINT('',(0.000877828539773374,0.004,0.00441354925822283));
#34592=CARTESIAN_POINT('',(0.,0.004,0.));
#34593=CARTESIAN_POINT('',(0.000877984358098221,0.004,0.00441351826403096));
#34594=CARTESIAN_POINT('',(0.0012940952255126,0.004,0.00482962913144534));
#34595=CARTESIAN_POINT('',(0.0012940952255126,0.004,0.00482962913144534));
#34596=CARTESIAN_POINT('',(0.0012940952255126,0.004,0.00482962913144534));
#34597=CARTESIAN_POINT('',(0.00144640237377705,0.004,0.00426121111576652));
#34598=CARTESIAN_POINT('',(0.,0.004,0.));
#34599=CARTESIAN_POINT('',(0.00144655281350068,0.004,0.00426116004836163));
#34600=CARTESIAN_POINT('',(0.00191341716182545,0.004,0.00461939766255643));
#34601=CARTESIAN_POINT('',(0.00191341716182545,0.004,0.00461939766255643));
#34602=CARTESIAN_POINT('',(0.00191341716182545,0.004,0.00461939766255643));
#34603=CARTESIAN_POINT('',(0.00199022786214689,0.004,0.00403596246968851));
#34604=CARTESIAN_POINT('',(0.,0.004,0.));
#34605=CARTESIAN_POINT('',(0.00199037034920393,0.004,0.00403589220284807));
#34606=CARTESIAN_POINT('',(0.0025,0.004,0.00433012701892219));
#34607=CARTESIAN_POINT('',(0.0025,0.004,0.00433012701892219));
#34608=CARTESIAN_POINT('',(0.0025,0.004,0.00433012701892219));
#34609=CARTESIAN_POINT('',(0.0025,0.004,0.00374165738677394));
#34610=CARTESIAN_POINT('',(0.,0.004,0.));
#34611=CARTESIAN_POINT('',(0.00250013209639738,0.004,0.00374156912278306));
#34612=CARTESIAN_POINT('',(0.0030438071450436,0.004,0.00396676670145617));
#34613=CARTESIAN_POINT('',(0.0030438071450436,0.004,0.00396676670145617));
#34614=CARTESIAN_POINT('',(0.0030438071450436,0.004,0.00396676670145617));
#34615=CARTESIAN_POINT('',(0.00296699644472216,0.004,0.00338333150858826));
#34616=CARTESIAN_POINT('',(0.,0.004,0.));
#34617=CARTESIAN_POINT('',(0.00296711589025392,0.004,0.00338322675766829));
#34618=CARTESIAN_POINT('',(0.00353553390593274,0.004,0.00353553390593274));
#34619=CARTESIAN_POINT('',(0.00353553390593274,0.004,0.00353553390593274));
#34620=CARTESIAN_POINT('',(0.00353553390593274,0.004,0.00353553390593274));
#34621=CARTESIAN_POINT('',(0.00338322675766829,0.004,0.00296711589025392));
#34622=CARTESIAN_POINT('',(0.,0.004,0.));
#34623=CARTESIAN_POINT('',(0.00338333150858826,0.004,0.00296699644472216));
#34624=CARTESIAN_POINT('',(0.00396676670145617,0.004,0.0030438071450436));
#34625=CARTESIAN_POINT('',(0.00396676670145617,0.004,0.0030438071450436));
#34626=CARTESIAN_POINT('',(0.00396676670145617,0.004,0.0030438071450436));
#34627=CARTESIAN_POINT('',(0.00374156912278307,0.004,0.00250013209639738));
#34628=CARTESIAN_POINT('',(0.,0.004,0.));
#34629=CARTESIAN_POINT('',(0.00374165738677394,0.004,0.0025));
#34630=CARTESIAN_POINT('',(0.00433012701892219,0.004,0.0025));
#34631=CARTESIAN_POINT('',(0.00433012701892219,0.004,0.0025));
#34632=CARTESIAN_POINT('',(0.00433012701892219,0.004,0.0025));
#34633=CARTESIAN_POINT('',(0.00403589220284807,0.004,0.00199037034920393));
#34634=CARTESIAN_POINT('',(0.,0.004,0.));
#34635=CARTESIAN_POINT('',(0.00403596246968851,0.004,0.00199022786214689));
#34636=CARTESIAN_POINT('',(0.00461939766255643,0.004,0.00191341716182545));
#34637=CARTESIAN_POINT('',(0.00461939766255643,0.004,0.00191341716182545));
#34638=CARTESIAN_POINT('',(0.00461939766255643,0.004,0.00191341716182545));
#34639=CARTESIAN_POINT('',(0.00426116004836162,0.004,0.00144655281350068));
#34640=CARTESIAN_POINT('',(0.,0.004,0.));
#34641=CARTESIAN_POINT('',(0.00426121111576652,0.004,0.00144640237377705));
#34642=CARTESIAN_POINT('',(0.00482962913144534,0.004,0.0012940952255126));
#34643=CARTESIAN_POINT('',(0.00482962913144534,0.004,0.0012940952255126));
#34644=CARTESIAN_POINT('',(0.00482962913144534,0.004,0.0012940952255126));
#34645=CARTESIAN_POINT('',(0.00441351826403096,0.004,0.000877984358098221));
#34646=CARTESIAN_POINT('',(0.,0.004,0.));
#34647=CARTESIAN_POINT('',(0.00441354925822283,0.004,0.000877828539773374));
#34648=CARTESIAN_POINT('',(0.00495722430686905,0.004,0.000652630961100258));
#34649=CARTESIAN_POINT('',(0.00495722430686905,0.004,0.000652630961100258));
#34650=CARTESIAN_POINT('',(0.00495722430686905,0.004,0.000652630961100258));
#34651=CARTESIAN_POINT('',(0.00449035995854428,0.004,0.000294393346905452));
#34652=CARTESIAN_POINT('',(0.,0.004,0.));
#34653=CARTESIAN_POINT('',(0.,0.004,0.));
#34654=CARTESIAN_POINT('',(0.,0.004,0.004));
#34655=CARTESIAN_POINT('',(0.,0.004,0.));
#34656=CARTESIAN_POINT('',(0.00449037034920393,0.004,0.000294234816074125));
#34657=CARTESIAN_POINT('',(0.00449035995854428,0.004,0.000294393346905452));
#34658=CARTESIAN_POINT('',(-0.00191341716182545,0.004,-0.00461939766255643));
#34659=CARTESIAN_POINT('',(0.00495722430686905,0.004,0.000652630961100258));
#34660=CARTESIAN_POINT('',(-0.0030438071450436,0.004,0.00396676670145617));
#34661=CARTESIAN_POINT('',(0.00441354925822283,0.004,0.000877828539773374));
#34662=CARTESIAN_POINT('',(0.,0.004,0.));
#34663=CARTESIAN_POINT('',(0.00441351826403096,0.004,0.000877984358098221));
#34664=CARTESIAN_POINT('',(-0.00129409522551261,0.004,-0.00482962913144534));
#34665=CARTESIAN_POINT('',(0.00482962913144534,0.004,0.0012940952255126));
#34666=CARTESIAN_POINT('',(-0.00353553390593274,0.004,0.00353553390593274));
#34667=CARTESIAN_POINT('',(0.00426121111576652,0.004,0.00144640237377705));
#34668=CARTESIAN_POINT('',(0.,0.004,0.));
#34669=CARTESIAN_POINT('',(0.00426116004836163,0.004,0.00144655281350068));
#34670=CARTESIAN_POINT('',(-0.000652630961100263,0.004,-0.00495722430686905));
#34671=CARTESIAN_POINT('',(0.00461939766255643,0.004,0.00191341716182545));
#34672=CARTESIAN_POINT('',(-0.00396676670145617,0.004,0.0030438071450436));
#34673=CARTESIAN_POINT('',(0.00403596246968851,0.004,0.00199022786214689));
#34674=CARTESIAN_POINT('',(0.,0.004,0.));
#34675=CARTESIAN_POINT('',(0.00403589220284807,0.004,0.00199037034920393));
#34676=CARTESIAN_POINT('',(-9.18485099360482E-19,0.004,-0.005));
#34677=CARTESIAN_POINT('',(0.00433012701892219,0.004,0.0025));
#34678=CARTESIAN_POINT('',(-0.00433012701892219,0.004,0.0025));
#34679=CARTESIAN_POINT('',(0.00374165738677394,0.004,0.0025));
#34680=CARTESIAN_POINT('',(0.,0.004,0.));
#34681=CARTESIAN_POINT('',(0.00374156912278306,0.004,0.00250013209639738));
#34682=CARTESIAN_POINT('',(0.000652630961100256,0.004,-0.00495722430686905));
#34683=CARTESIAN_POINT('',(0.00396676670145617,0.004,0.0030438071450436));
#34684=CARTESIAN_POINT('',(-0.00461939766255643,0.004,0.00191341716182545));
#34685=CARTESIAN_POINT('',(0.00338333150858826,0.004,0.00296699644472216));
#34686=CARTESIAN_POINT('',(0.,0.004,0.));
#34687=CARTESIAN_POINT('',(0.00338322675766829,0.004,0.00296711589025392));
#34688=CARTESIAN_POINT('',(0.00353553390593274,0.004,0.00353553390593274));
#34689=CARTESIAN_POINT('',(0.00353553390593274,0.004,0.00353553390593274));
#34690=CARTESIAN_POINT('',(-0.00482962913144534,0.004,0.0012940952255126));
#34691=CARTESIAN_POINT('',(0.00296711589025392,0.004,0.00338322675766829));
#34692=CARTESIAN_POINT('',(0.,0.004,0.));
#34693=CARTESIAN_POINT('',(0.00296699644472216,0.004,0.00338333150858826));
#34694=CARTESIAN_POINT('',(0.0030438071450436,0.004,0.00396676670145617));
#34695=CARTESIAN_POINT('',(0.0030438071450436,0.004,0.00396676670145617));
#34696=CARTESIAN_POINT('',(-0.00495722430686905,0.004,0.00065263096110026));
#34697=CARTESIAN_POINT('',(0.00250013209639738,0.004,0.00374156912278306));
#34698=CARTESIAN_POINT('',(0.,0.004,0.));
#34699=CARTESIAN_POINT('',(0.0025,0.004,0.00374165738677394));
#34700=CARTESIAN_POINT('',(0.0025,0.004,0.00433012701892219));
#34701=CARTESIAN_POINT('',(0.0025,0.004,0.00433012701892219));
#34702=CARTESIAN_POINT('',(-0.005,0.004,6.12323399573786E-19));
#34703=CARTESIAN_POINT('',(0.00199037034920393,0.004,0.00403589220284807));
#34704=CARTESIAN_POINT('',(0.,0.004,0.));
#34705=CARTESIAN_POINT('',(0.00199022786214689,0.004,0.00403596246968851));
#34706=CARTESIAN_POINT('',(0.00191341716182545,0.004,0.00461939766255643));
#34707=CARTESIAN_POINT('',(0.00191341716182545,0.004,0.00461939766255643));
#34708=CARTESIAN_POINT('',(-0.00495722430686905,0.004,-0.000652630961100257));
#34709=CARTESIAN_POINT('',(0.00144655281350068,0.004,0.00426116004836163));
#34710=CARTESIAN_POINT('',(0.,0.004,0.));
#34711=CARTESIAN_POINT('',(0.00144640237377705,0.004,0.00426121111576652));
#34712=CARTESIAN_POINT('',(0.0012940952255126,0.004,0.00482962913144534));
#34713=CARTESIAN_POINT('',(0.0012940952255126,0.004,0.00482962913144534));
#34714=CARTESIAN_POINT('',(-0.00482962913144534,0.004,-0.0012940952255126));
#34715=CARTESIAN_POINT('',(0.000877984358098221,0.004,0.00441351826403096));
#34716=CARTESIAN_POINT('',(0.,0.004,0.));
#34717=CARTESIAN_POINT('',(0.000877828539773374,0.004,0.00441354925822283));
#34718=CARTESIAN_POINT('',(0.000652630961100259,0.004,0.00495722430686905));
#34719=CARTESIAN_POINT('',(0.000652630961100259,0.004,0.00495722430686905));
#34720=CARTESIAN_POINT('',(-0.00461939766255644,0.004,-0.00191341716182544));
#34721=CARTESIAN_POINT('',(0.000294393346905451,0.004,0.00449035995854428));
#34722=CARTESIAN_POINT('',(0.,0.004,0.));
#34723=CARTESIAN_POINT('',(0.000294234816074127,0.004,0.00449037034920393));
#34724=CARTESIAN_POINT('',(3.06161699786893E-19,0.004,0.005));
#34725=CARTESIAN_POINT('',(3.06161699786893E-19,0.004,0.005));
#34726=CARTESIAN_POINT('',(-0.00433012701892219,0.004,-0.0025));
#34727=CARTESIAN_POINT('',(-0.000294234816074129,0.004,0.00449037034920393));
#34728=CARTESIAN_POINT('',(0.,0.004,0.));
#34729=CARTESIAN_POINT('',(-0.000294393346905451,0.004,0.00449035995854428));
#34730=CARTESIAN_POINT('',(-0.000652630961100257,0.004,0.00495722430686905));
#34731=CARTESIAN_POINT('',(-0.000652630961100257,0.004,0.00495722430686905));
#34732=CARTESIAN_POINT('',(-0.00396676670145617,0.004,-0.0030438071450436));
#34733=CARTESIAN_POINT('',(-0.000877828539773375,0.004,0.00441354925822283));
#34734=CARTESIAN_POINT('',(0.,0.004,0.));
#34735=CARTESIAN_POINT('',(-0.000877984358098221,0.004,0.00441351826403096));
#34736=CARTESIAN_POINT('',(-0.0012940952255126,0.004,0.00482962913144534));
#34737=CARTESIAN_POINT('',(-0.0012940952255126,0.004,0.00482962913144534));
#34738=CARTESIAN_POINT('',(-0.0012940952255126,0.004,0.00482962913144534));
#34739=CARTESIAN_POINT('',(-0.00144640237377705,0.004,0.00426121111576652));
#34740=CARTESIAN_POINT('',(0.,0.004,0.));
#34741=CARTESIAN_POINT('',(-0.00144655281350068,0.004,0.00426116004836163));
#34742=CARTESIAN_POINT('',(-0.00191341716182545,0.004,0.00461939766255643));
#34743=CARTESIAN_POINT('',(-0.00191341716182545,0.004,0.00461939766255643));
#34744=CARTESIAN_POINT('',(-0.00191341716182545,0.004,0.00461939766255643));
#34745=CARTESIAN_POINT('',(-0.00199022786214689,0.004,0.00403596246968851));
#34746=CARTESIAN_POINT('',(0.,0.004,0.));
#34747=CARTESIAN_POINT('',(-0.00199037034920393,0.004,0.00403589220284807));
#34748=CARTESIAN_POINT('',(-0.0025,0.004,0.00433012701892219));
#34749=CARTESIAN_POINT('',(-0.0025,0.004,0.00433012701892219));
#34750=CARTESIAN_POINT('',(-0.0025,0.004,0.00433012701892219));
#34751=CARTESIAN_POINT('',(-0.0025,0.004,0.00374165738677394));
#34752=CARTESIAN_POINT('',(0.,0.004,0.));
#34753=CARTESIAN_POINT('',(-0.00250013209639738,0.004,0.00374156912278307));
#34754=CARTESIAN_POINT('',(-0.0030438071450436,0.004,0.00396676670145617));
#34755=CARTESIAN_POINT('',(-0.0030438071450436,0.004,0.00396676670145617));
#34756=CARTESIAN_POINT('',(-0.0030438071450436,0.004,0.00396676670145617));
#34757=CARTESIAN_POINT('',(-0.00296699644472215,0.004,0.00338333150858826));
#34758=CARTESIAN_POINT('',(0.,0.004,0.));
#34759=CARTESIAN_POINT('',(-0.00296711589025392,0.004,0.00338322675766829));
#34760=CARTESIAN_POINT('',(-0.00353553390593274,0.004,0.00353553390593274));
#34761=CARTESIAN_POINT('',(-0.00353553390593274,0.004,0.00353553390593274));
#34762=CARTESIAN_POINT('',(-0.00353553390593274,0.004,0.00353553390593274));
#34763=CARTESIAN_POINT('',(-0.0033832267576683,0.004,0.00296711589025391));
#34764=CARTESIAN_POINT('',(0.,0.004,0.));
#34765=CARTESIAN_POINT('',(-0.00338333150858826,0.004,0.00296699644472216));
#34766=CARTESIAN_POINT('',(-0.00396676670145617,0.004,0.0030438071450436));
#34767=CARTESIAN_POINT('',(-0.00396676670145617,0.004,0.0030438071450436));
#34768=CARTESIAN_POINT('',(-0.00396676670145617,0.004,0.0030438071450436));
#34769=CARTESIAN_POINT('',(-0.00374156912278306,0.004,0.00250013209639738));
#34770=CARTESIAN_POINT('',(0.,0.004,0.));
#34771=CARTESIAN_POINT('',(-0.00374165738677394,0.004,0.0025));
#34772=CARTESIAN_POINT('',(-0.00433012701892219,0.004,0.0025));
#34773=CARTESIAN_POINT('',(-0.00433012701892219,0.004,0.0025));
#34774=CARTESIAN_POINT('',(-0.00433012701892219,0.004,0.0025));
#34775=CARTESIAN_POINT('',(-0.00403589220284807,0.004,0.00199037034920393));
#34776=CARTESIAN_POINT('',(0.,0.004,0.));
#34777=CARTESIAN_POINT('',(-0.00403596246968851,0.004,0.00199022786214689));
#34778=CARTESIAN_POINT('',(-0.00461939766255643,0.004,0.00191341716182545));
#34779=CARTESIAN_POINT('',(-0.00461939766255643,0.004,0.00191341716182545));
#34780=CARTESIAN_POINT('',(-0.00461939766255643,0.004,0.00191341716182545));
#34781=CARTESIAN_POINT('',(-0.00426116004836163,0.004,0.00144655281350067));
#34782=CARTESIAN_POINT('',(0.,0.004,0.));
#34783=CARTESIAN_POINT('',(-0.00426121111576652,0.004,0.00144640237377705));
#34784=CARTESIAN_POINT('',(-0.00482962913144534,0.004,0.0012940952255126));
#34785=CARTESIAN_POINT('',(-0.00482962913144534,0.004,0.0012940952255126));
#34786=CARTESIAN_POINT('',(-0.00482962913144534,0.004,0.0012940952255126));
#34787=CARTESIAN_POINT('',(-0.00441351826403096,0.004,0.000877984358098221));
#34788=CARTESIAN_POINT('',(0.,0.004,0.));
#34789=CARTESIAN_POINT('',(-0.00441354925822283,0.004,0.000877828539773375));
#34790=CARTESIAN_POINT('',(-0.00495722430686905,0.004,0.00065263096110026));
#34791=CARTESIAN_POINT('',(-0.00495722430686905,0.004,0.00065263096110026));
#34792=CARTESIAN_POINT('',(-0.00495722430686905,0.004,0.00065263096110026));
#34793=CARTESIAN_POINT('',(-0.00449035995854428,0.004,0.000294393346905453));
#34794=CARTESIAN_POINT('',(0.,0.004,0.));
#34795=CARTESIAN_POINT('',(-0.00449037034920393,0.004,0.000294234816074127));
#34796=CARTESIAN_POINT('',(-0.005,0.004,6.12323399573786E-19));
#34797=CARTESIAN_POINT('',(-0.005,0.004,6.12323399573786E-19));
#34798=CARTESIAN_POINT('',(-0.005,0.004,6.12323399573786E-19));
#34799=CARTESIAN_POINT('',(-0.00449037034920393,0.004,-0.000294234816074129));
#34800=CARTESIAN_POINT('',(0.,0.004,0.));
#34801=CARTESIAN_POINT('',(-0.00449035995854428,0.004,-0.000294393346905451));
#34802=CARTESIAN_POINT('',(-0.00495722430686905,0.004,-0.000652630961100257));
#34803=CARTESIAN_POINT('',(-0.00495722430686905,0.004,-0.000652630961100257));
#34804=CARTESIAN_POINT('',(-0.00495722430686905,0.004,-0.000652630961100257));
#34805=CARTESIAN_POINT('',(-0.00441354925822283,0.004,-0.000877828539773375));
#34806=CARTESIAN_POINT('',(0.,0.004,0.));
#34807=CARTESIAN_POINT('',(-0.00441351826403096,0.004,-0.00087798435809822));
#34808=CARTESIAN_POINT('',(-0.00482962913144534,0.004,-0.0012940952255126));
#34809=CARTESIAN_POINT('',(-0.00482962913144534,0.004,-0.0012940952255126));
#34810=CARTESIAN_POINT('',(-0.00482962913144534,0.004,-0.0012940952255126));
#34811=CARTESIAN_POINT('',(-0.00426121111576652,0.004,-0.00144640237377705));
#34812=CARTESIAN_POINT('',(0.,0.004,0.));
#34813=CARTESIAN_POINT('',(-0.00426116004836163,0.004,-0.00144655281350068));
#34814=CARTESIAN_POINT('',(-0.00461939766255644,0.004,-0.00191341716182544));
#34815=CARTESIAN_POINT('',(-0.00461939766255644,0.004,-0.00191341716182544));
#34816=CARTESIAN_POINT('',(-0.00461939766255644,0.004,-0.00191341716182544));
#34817=CARTESIAN_POINT('',(-0.00403596246968851,0.004,-0.00199022786214689));
#34818=CARTESIAN_POINT('',(0.,0.004,0.));
#34819=CARTESIAN_POINT('',(-0.00403589220284807,0.004,-0.00199037034920393));
#34820=CARTESIAN_POINT('',(-0.00433012701892219,0.004,-0.0025));
#34821=CARTESIAN_POINT('',(-0.00433012701892219,0.004,-0.0025));
#34822=CARTESIAN_POINT('',(-0.00433012701892219,0.004,-0.0025));
#34823=CARTESIAN_POINT('',(-0.00374165738677394,0.004,-0.0025));
#34824=CARTESIAN_POINT('',(0.,0.004,0.));
#34825=CARTESIAN_POINT('',(-0.00374156912278307,0.004,-0.00250013209639738));
#34826=CARTESIAN_POINT('',(-0.00396676670145617,0.004,-0.0030438071450436));
#34827=CARTESIAN_POINT('',(-0.00396676670145617,0.004,-0.0030438071450436));
#34828=CARTESIAN_POINT('',(-0.00396676670145617,0.004,-0.0030438071450436));
#34829=CARTESIAN_POINT('',(-0.00338333150858826,0.004,-0.00296699644472216));
#34830=CARTESIAN_POINT('',(0.,0.004,0.));
#34831=CARTESIAN_POINT('',(-0.0033832267576683,0.004,-0.00296711589025391));
#34832=CARTESIAN_POINT('',(-0.0012940952255126,0.004,0.00482962913144534));
#34833=CARTESIAN_POINT('',(-0.00353553390593274,0.004,-0.00353553390593274));
#34834=CARTESIAN_POINT('',(-0.00353553390593274,0.004,-0.00353553390593274));
#34835=CARTESIAN_POINT('',(-0.00296711589025392,0.004,-0.00338322675766829));
#34836=CARTESIAN_POINT('',(0.,0.004,0.));
#34837=CARTESIAN_POINT('',(-0.00296699644472216,0.004,-0.00338333150858826));
#34838=CARTESIAN_POINT('',(-0.00191341716182545,0.004,0.00461939766255643));
#34839=CARTESIAN_POINT('',(-0.0030438071450436,0.004,-0.00396676670145617));
#34840=CARTESIAN_POINT('',(-0.0030438071450436,0.004,-0.00396676670145617));
#34841=CARTESIAN_POINT('',(-0.00250013209639738,0.004,-0.00374156912278306));
#34842=CARTESIAN_POINT('',(0.,0.004,0.));
#34843=CARTESIAN_POINT('',(-0.0025,0.004,-0.00374165738677394));
#34844=CARTESIAN_POINT('',(-0.0025,0.004,0.00433012701892219));
#34845=CARTESIAN_POINT('',(-0.0025,0.004,-0.00433012701892219));
#34846=CARTESIAN_POINT('',(-0.0025,0.004,-0.00433012701892219));
#34847=CARTESIAN_POINT('',(-0.00199037034920393,0.004,-0.00403589220284807));
#34848=CARTESIAN_POINT('',(0.,0.004,0.));
#34849=CARTESIAN_POINT('',(-0.0019902278621469,0.004,-0.00403596246968851));
#34850=CARTESIAN_POINT('',(-0.0030438071450436,0.004,0.00396676670145617));
#34851=CARTESIAN_POINT('',(-0.00191341716182545,0.004,-0.00461939766255643));
#34852=CARTESIAN_POINT('',(-0.00191341716182545,0.004,-0.00461939766255643));
#34853=CARTESIAN_POINT('',(-0.00144655281350068,0.004,-0.00426116004836162));
#34854=CARTESIAN_POINT('',(0.,0.004,0.));
#34855=CARTESIAN_POINT('',(-0.00144640237377705,0.004,-0.00426121111576652));
#34856=CARTESIAN_POINT('',(-0.00353553390593274,0.004,0.00353553390593274));
#34857=CARTESIAN_POINT('',(-0.00129409522551261,0.004,-0.00482962913144534));
#34858=CARTESIAN_POINT('',(-0.00129409522551261,0.004,-0.00482962913144534));
#34859=CARTESIAN_POINT('',(-0.000877984358098222,0.004,-0.00441351826403096));
#34860=CARTESIAN_POINT('',(0.,0.004,0.));
#34861=CARTESIAN_POINT('',(-0.000877828539773377,0.004,-0.00441354925822283));
#34862=CARTESIAN_POINT('',(-0.00396676670145617,0.004,0.0030438071450436));
#34863=CARTESIAN_POINT('',(-0.000652630961100263,0.004,-0.00495722430686905));
#34864=CARTESIAN_POINT('',(-0.000652630961100263,0.004,-0.00495722430686905));
#34865=CARTESIAN_POINT('',(-0.000294393346905453,0.004,-0.00449035995854428));
#34866=CARTESIAN_POINT('',(0.,0.004,0.));
#34867=CARTESIAN_POINT('',(-0.000294234816074127,0.004,-0.00449037034920393));
#34868=CARTESIAN_POINT('',(-0.00433012701892219,0.004,0.0025));
#34869=CARTESIAN_POINT('',(-9.18485099360482E-19,0.004,-0.005));
#34870=CARTESIAN_POINT('',(-9.18485099360482E-19,0.004,-0.005));
#34871=CARTESIAN_POINT('',(0.000294234816074127,0.004,-0.00449037034920393));
#34872=CARTESIAN_POINT('',(0.,0.004,0.));
#34873=CARTESIAN_POINT('',(0.000294393346905451,0.004,-0.00449035995854428));
#34874=CARTESIAN_POINT('',(-0.00461939766255643,0.004,0.00191341716182545));
#34875=CARTESIAN_POINT('',(0.000652630961100256,0.004,-0.00495722430686905));
#34876=CARTESIAN_POINT('',(0.000652630961100256,0.004,-0.00495722430686905));
#34877=CARTESIAN_POINT('',(0.000877828539773373,0.004,-0.00441354925822283));
#34878=CARTESIAN_POINT('',(0.,0.004,0.));
#34879=CARTESIAN_POINT('',(0.000877984358098219,0.004,-0.00441351826403096));
#34880=CARTESIAN_POINT('',(-0.00482962913144534,0.004,0.0012940952255126));
#34881=CARTESIAN_POINT('',(0.0012940952255126,0.004,-0.00482962913144534));
#34882=CARTESIAN_POINT('',(0.00353553390593274,0.004,0.00353553390593274));
#34883=CARTESIAN_POINT('',(0.00144640237377704,0.004,-0.00426121111576652));
#34884=CARTESIAN_POINT('',(0.,0.004,0.));
#34885=CARTESIAN_POINT('',(0.00144655281350068,0.004,-0.00426116004836163));
#34886=CARTESIAN_POINT('',(-0.00495722430686905,0.004,0.00065263096110026));
#34887=CARTESIAN_POINT('',(0.00191341716182544,0.004,-0.00461939766255644));
#34888=CARTESIAN_POINT('',(0.0030438071450436,0.004,0.00396676670145617));
#34889=CARTESIAN_POINT('',(0.00199022786214689,0.004,-0.00403596246968851));
#34890=CARTESIAN_POINT('',(0.,0.004,0.));
#34891=CARTESIAN_POINT('',(0.00199037034920392,0.004,-0.00403589220284807));
#34892=CARTESIAN_POINT('',(-0.005,0.004,6.12323399573786E-19));
#34893=CARTESIAN_POINT('',(0.0025,0.004,-0.00433012701892219));
#34894=CARTESIAN_POINT('',(0.0025,0.004,0.00433012701892219));
#34895=CARTESIAN_POINT('',(0.0025,0.004,-0.00374165738677394));
#34896=CARTESIAN_POINT('',(0.,0.004,0.));
#34897=CARTESIAN_POINT('',(0.00250013209639738,0.004,-0.00374156912278307));
#34898=CARTESIAN_POINT('',(-0.00495722430686905,0.004,-0.000652630961100257));
#34899=CARTESIAN_POINT('',(0.0030438071450436,0.004,-0.00396676670145618));
#34900=CARTESIAN_POINT('',(0.00191341716182545,0.004,0.00461939766255643));
#34901=CARTESIAN_POINT('',(0.00296699644472215,0.004,-0.00338333150858826));
#34902=CARTESIAN_POINT('',(0.,0.004,0.));
#34903=CARTESIAN_POINT('',(0.00296711589025392,0.004,-0.00338322675766829));
#34904=CARTESIAN_POINT('',(-0.00482962913144534,0.004,-0.0012940952255126));
#34905=CARTESIAN_POINT('',(0.00353553390593274,0.004,-0.00353553390593274));
#34906=CARTESIAN_POINT('',(0.0012940952255126,0.004,0.00482962913144534));
#34907=CARTESIAN_POINT('',(0.00338322675766829,0.004,-0.00296711589025392));
#34908=CARTESIAN_POINT('',(0.,0.004,0.));
#34909=CARTESIAN_POINT('',(0.00338333150858826,0.004,-0.00296699644472216));
#34910=CARTESIAN_POINT('',(-0.00461939766255644,0.004,-0.00191341716182544));
#34911=CARTESIAN_POINT('',(0.00396676670145617,0.004,-0.0030438071450436));
#34912=CARTESIAN_POINT('',(0.00396676670145617,0.004,-0.0030438071450436));
#34913=CARTESIAN_POINT('',(0.00374165738677394,0.004,-0.0025));
#34914=CARTESIAN_POINT('',(-0.00433012701892219,0.004,-0.0025));
#34915=CARTESIAN_POINT('',(0.00433012701892219,0.004,-0.0025));
#34916=CARTESIAN_POINT('',(3.06161699786893E-19,0.004,0.005));
#34917=CARTESIAN_POINT('',(0.00403589220284806,0.004,-0.00199037034920393));
#34918=CARTESIAN_POINT('',(0.,0.004,0.));
#34919=CARTESIAN_POINT('',(0.00403596246968851,0.004,-0.0019902278621469));
#34920=CARTESIAN_POINT('',(-0.00396676670145617,0.004,-0.0030438071450436));
#34921=CARTESIAN_POINT('',(0.00461939766255643,0.004,-0.00191341716182545));
#34922=CARTESIAN_POINT('',(-0.000652630961100257,0.004,0.00495722430686905));
#34923=CARTESIAN_POINT('',(0.00426116004836162,0.004,-0.00144655281350068));
#34924=CARTESIAN_POINT('',(0.,0.004,0.));
#34925=CARTESIAN_POINT('',(0.00426121111576652,0.004,-0.00144640237377705));
#34926=CARTESIAN_POINT('',(-0.00353553390593274,0.004,-0.00353553390593274));
#34927=CARTESIAN_POINT('',(0.00482962913144534,0.004,-0.00129409522551261));
#34928=CARTESIAN_POINT('',(-0.0012940952255126,0.004,0.00482962913144534));
#34929=CARTESIAN_POINT('',(0.00441351826403096,0.004,-0.000877984358098224));
#34930=CARTESIAN_POINT('',(0.,0.004,0.));
#34931=CARTESIAN_POINT('',(0.00441354925822283,0.004,-0.000877828539773378));
#34932=CARTESIAN_POINT('',(-0.0030438071450436,0.004,-0.00396676670145617));
#34933=CARTESIAN_POINT('',(0.00495722430686905,0.004,-0.000652630961100263));
#34934=CARTESIAN_POINT('',(-0.00191341716182545,0.004,0.00461939766255643));
#34935=CARTESIAN_POINT('',(0.00449035995854428,0.004,-0.000294393346905455));
#34936=CARTESIAN_POINT('',(0.,0.004,0.));
#34937=CARTESIAN_POINT('',(0.00449037034920393,0.004,-0.000294234816074128));
#34938=CARTESIAN_POINT('',(-0.0025,0.004,-0.00433012701892219));
#34939=CARTESIAN_POINT('',(0.005,0.004,0.));
#34940=CARTESIAN_POINT('',(-0.0025,0.004,0.00433012701892219));
#34941=CARTESIAN_POINT('',(0.,0.006,0.));
#34942=CARTESIAN_POINT('',(0.,0.006,0.));
#34943=CARTESIAN_POINT('',(0.,0.006,0.));
#34944=CARTESIAN_POINT('',(0.,0.006,0.004));
#34945=CARTESIAN_POINT('',(0.,0.012,0.));
#34946=CARTESIAN_POINT('',(0.,0.006,0.));
#34947=CARTESIAN_POINT('',(0.,0.001,0.));
#34948=CARTESIAN_POINT('',(0.,3.17541634481466E-5,0.));
#34949=CARTESIAN_POINT('',(0.,3.17541634481466E-5,0.00025));
#34950=CARTESIAN_POINT('',(0.,0.022,0.));
#34951=CARTESIAN_POINT('',(0.,0.011,0.));
#34952=CARTESIAN_POINT('',(0.,0.011,0.001));
#34953=CARTESIAN_POINT('',(0.,0.011,0.));
#34954=CARTESIAN_POINT('',(0.,3.17541634481466E-5,0.));
#45463=MECHANICAL_DESIGN_GEOMETRIC_PRESENTATION_REPRESENTATION('',(#13540),#45464);
#45464=(
GEOMETRIC_REPRESENTATION_CONTEXT(3)
GLOBAL_UNCERTAINTY_ASSIGNED_CONTEXT((#45492))
GLOBAL_UNIT_ASSIGNED_CONTEXT((#45522,#45521,#45520))
REPRESENTATION_CONTEXT('MAS-690','TOP_LEVEL_ASSEMBLY_PART')
);
#45476=(
GEOMETRIC_REPRESENTATION_CONTEXT(3)
GLOBAL_UNCERTAINTY_ASSIGNED_CONTEXT((#45504))
GLOBAL_UNIT_ASSIGNED_CONTEXT((#45522,#45521,#45520))
REPRESENTATION_CONTEXT('Nozzle cap','COMPONENT_PART')
);
#45492=UNCERTAINTY_MEASURE_WITH_UNIT(LENGTH_MEASURE(1.E-8),#45522,
'DISTANCE_ACCURACY_VALUE','Maximum Tolerance applied to model');
#45504=UNCERTAINTY_MEASURE_WITH_UNIT(LENGTH_MEASURE(2.E-5),#45522,
'DISTANCE_ACCURACY_VALUE','Maximum Tolerance applied to model');
#45520=(
NAMED_UNIT(*)
SI_UNIT($,.STERADIAN.)
SOLID_ANGLE_UNIT()
);
#45521=(
NAMED_UNIT(*)
PLANE_ANGLE_UNIT()
SI_UNIT($,.RADIAN.)
);
#45522=(
LENGTH_UNIT()
NAMED_UNIT(*)
SI_UNIT($,.METRE.)
);
#45548=PRODUCT_DEFINITION_SHAPE('','',#45597);
#45597=PRODUCT_DEFINITION('','',#45653,#45625);
#45625=PRODUCT_DEFINITION_CONTEXT('',#45782,'design');
#45653=PRODUCT_DEFINITION_FORMATION_WITH_SPECIFIED_SOURCE('','',#45709,
 .NOT_KNOWN.);
#45709=PRODUCT('Nozzle cap','Nozzle cap','Nozzle cap',(#45765));
#45765=PRODUCT_CONTEXT('',#45782,'mechanical');
#45782=APPLICATION_CONTEXT('managed model based 3d engineering');
ENDSEC;
END-ISO-10303-21;
